ISO-10303-21;
HEADER;
/* Generated by software containing ST-Developer
 * from STEP Tools, Inc. (www.steptools.com) 
 */

FILE_DESCRIPTION(
/* description */ (''),
/* implementation_level */ '2;1');

FILE_NAME(
/* name */ 'Hex nut M3.step',
/* time_stamp */ '2026-11-10T09:05:57-08:00',
/* author */ (''),
/* organization */ (''),
/* preprocessor_version */ 'ST-DEVELOPER v20.2',
/* originating_system */ 'Autodesk Translation Framework v15.17.0.0',
/* authorisation */ '');

FILE_SCHEMA (('AUTOMOTIVE_DESIGN { 1 0 10303 214 3 1 1 }'));
ENDSEC;

DATA;
#10=MECHANICAL_DESIGN_GEOMETRIC_PRESENTATION_REPRESENTATION('',(#573),#19618);
#169=B_SPLINE_SURFACE_WITH_KNOTS('',3,3,((#18989,#18990,#18991,#18992,#18993,
#18994,#18995,#18996,#18997,#18998,#18999,#19000,#19001,#19002,#19003,#19004,
#19005,#19006,#19007,#19008,#19009,#19010,#19011,#19012,#19013,#19014,#19015,
#19016,#19017,#19018,#19019,#19020,#19021,#19022,#19023,#19024),(#19025,
#19026,#19027,#19028,#19029,#19030,#19031,#19032,#19033,#19034,#19035,#19036,
#19037,#19038,#19039,#19040,#19041,#19042,#19043,#19044,#19045,#19046,#19047,
#19048,#19049,#19050,#19051,#19052,#19053,#19054,#19055,#19056,#19057,#19058,
#19059,#19060),(#19061,#19062,#19063,#19064,#19065,#19066,#19067,#19068,
#19069,#19070,#19071,#19072,#19073,#19074,#19075,#19076,#19077,#19078,#19079,
#19080,#19081,#19082,#19083,#19084,#19085,#19086,#19087,#19088,#19089,#19090,
#19091,#19092,#19093,#19094,#19095,#19096),(#19097,#19098,#19099,#19100,
#19101,#19102,#19103,#19104,#19105,#19106,#19107,#19108,#19109,#19110,#19111,
#19112,#19113,#19114,#19115,#19116,#19117,#19118,#19119,#19120,#19121,#19122,
#19123,#19124,#19125,#19126,#19127,#19128,#19129,#19130,#19131,#19132)),
 .UNSPECIFIED.,.F.,.F.,.F.,(4,4),(4,1,1,1,1,1,1,1,1,1,1,1,1,1,1,1,1,1,1,
1,1,1,1,1,1,1,1,1,1,1,1,1,1,4),(0.,0.0321584099938622),(11.8553612635794,
12.830508595889,13.8056559281987,14.7808032605084,15.755950592818,16.7310979251277,
17.7062452574374,18.681392589747,19.6565399220567,20.6316872543664,21.606834586676,
22.5819819189857,23.5571292512954,24.532276583605,25.5074239159147,26.4825712482243,
27.457718580534,28.4328659128437,29.4080132451533,30.383160577463,31.3583079097727,
32.3334552420823,33.308602574392,34.2837499067017,35.2588972390113,36.234044571321,
37.2091919036307,38.1843392359403,39.15948656825,40.1346339005596,41.1097812328693,
42.084928565179,43.0600758974886,44.0352232297983),.UNSPECIFIED.);
#170=B_SPLINE_SURFACE_WITH_KNOTS('',3,3,((#19256,#19257,#19258,#19259,#19260,
#19261,#19262,#19263,#19264,#19265,#19266,#19267,#19268,#19269,#19270,#19271,
#19272,#19273,#19274,#19275,#19276,#19277,#19278,#19279,#19280,#19281,#19282,
#19283,#19284,#19285,#19286,#19287,#19288,#19289,#19290,#19291),(#19292,
#19293,#19294,#19295,#19296,#19297,#19298,#19299,#19300,#19301,#19302,#19303,
#19304,#19305,#19306,#19307,#19308,#19309,#19310,#19311,#19312,#19313,#19314,
#19315,#19316,#19317,#19318,#19319,#19320,#19321,#19322,#19323,#19324,#19325,
#19326,#19327),(#19328,#19329,#19330,#19331,#19332,#19333,#19334,#19335,
#19336,#19337,#19338,#19339,#19340,#19341,#19342,#19343,#19344,#19345,#19346,
#19347,#19348,#19349,#19350,#19351,#19352,#19353,#19354,#19355,#19356,#19357,
#19358,#19359,#19360,#19361,#19362,#19363),(#19364,#19365,#19366,#19367,
#19368,#19369,#19370,#19371,#19372,#19373,#19374,#19375,#19376,#19377,#19378,
#19379,#19380,#19381,#19382,#19383,#19384,#19385,#19386,#19387,#19388,#19389,
#19390,#19391,#19392,#19393,#19394,#19395,#19396,#19397,#19398,#19399)),
 .UNSPECIFIED.,.F.,.F.,.F.,(4,4),(4,1,1,1,1,1,1,1,1,1,1,1,1,1,1,1,1,1,1,
1,1,1,1,1,1,1,1,1,1,1,1,1,1,4),(0.,0.0321584099938622),(14.3984001269719,
15.3735474592815,16.3486947915912,17.3238421239009,18.2989894562105,19.2741367885202,
20.2492841208299,21.2244314531395,22.1995787854492,23.1747261177589,24.1498734500685,
25.1250207823782,26.1001681146879,27.0753154469975,28.0504627793072,29.0256101116168,
30.0007574439265,30.9759047762362,31.9510521085458,32.9261994408555,33.9013467731652,
34.8764941054748,35.8516414377845,36.8267887700942,37.8019361024038,38.7770834347135,
39.7522307670232,40.7273780993328,41.7025254316425,42.6776727639522,43.6528200962618,
44.6279674285715,45.6031147608811,46.5782620931908),.UNSPECIFIED.);
#518=B_SPLINE_CURVE_WITH_KNOTS('',3,(#18659,#18660,#18661,#18662,#18663,
#18664,#18665),.UNSPECIFIED.,.F.,.F.,(4,3,4),(-30.159289474462,-29.2544199692899,
-28.9853432330879),.UNSPECIFIED.);
#519=B_SPLINE_CURVE_WITH_KNOTS('',3,(#18671,#18672,#18673,#18674,#18675,
#18676,#18677,#18678,#18679,#18680,#18681,#18682,#18683,#18684,#18685,#18686,
#18687,#18688,#18689),.UNSPECIFIED.,.F.,.F.,(4,3,3,3,3,3,4),(26.4423043696954,
27.3041253046706,28.2792726369803,29.25441996929,30.2295673015996,31.2047146339093,
32.179861966219),.UNSPECIFIED.);
#520=B_SPLINE_CURVE_WITH_KNOTS('',3,(#18691,#18692,#18693,#18694,#18695,
#18696,#18697,#18698,#18699,#18700,#18701,#18702,#18703,#18704,#18705,#18706,
#18707,#18708,#18709,#18710,#18711,#18712),.UNSPECIFIED.,.F.,.F.,(4,3,3,
3,3,3,3,4),(-28.9853432330879,-28.2792726369803,-27.3041253046706,-26.3289779723609,
-25.3538306400513,-24.3786833077416,-23.403535975432,-22.7021579259084),
 .UNSPECIFIED.);
#521=B_SPLINE_CURVE_WITH_KNOTS('',3,(#18717,#18718,#18719,#18720,#18721,
#18722,#18723,#18724,#18725,#18726,#18727,#18728,#18729,#18730,#18731,#18732,
#18733,#18734,#18735,#18736,#18737,#18738,#18739,#18740,#18741),
 .UNSPECIFIED.,.F.,.F.,(4,3,3,3,3,3,3,3,4),(20.1591190625159,20.478093978503,
21.4532413108126,22.4283886431223,23.403535975432,24.3786833077416,25.3538306400513,
26.328977972361,26.4423043696954),.UNSPECIFIED.);
#522=B_SPLINE_CURVE_WITH_KNOTS('',3,(#18742,#18743,#18744,#18745,#18746,
#18747,#18748,#18749,#18750,#18751,#18752,#18753,#18754,#18755,#18756,#18757,
#18758,#18759,#18760,#18761,#18762,#18763,#18764,#18765,#18766),
 .UNSPECIFIED.,.F.,.F.,(4,3,3,3,3,3,3,3,4),(-22.7021579259084,-22.4283886431223,
-21.4532413108126,-20.478093978503,-19.5029466461933,-18.5277993138836,
-17.552651981574,-16.5775046492643,-16.4189726187288),.UNSPECIFIED.);
#523=B_SPLINE_CURVE_WITH_KNOTS('',3,(#18771,#18772,#18773,#18774,#18775,
#18776,#18777,#18778,#18779,#18780,#18781,#18782,#18783,#18784,#18785,#18786,
#18787,#18788,#18789,#18790,#18791,#18792),.UNSPECIFIED.,.F.,.F.,(4,3,3,
3,3,3,3,4),(13.8759337553363,14.627209984645,15.6023573169546,16.5775046492643,
17.552651981574,18.5277993138836,19.5029466461933,20.1591190625159),
 .UNSPECIFIED.);
#524=B_SPLINE_CURVE_WITH_KNOTS('',3,(#18793,#18794,#18795,#18796,#18797,
#18798,#18799,#18800,#18801,#18802,#18803,#18804,#18805,#18806,#18807,#18808,
#18809,#18810,#18811,#18812,#18813,#18814),.UNSPECIFIED.,.F.,.F.,(4,3,3,
3,3,3,3,4),(-16.4189726187288,-15.6023573169546,-14.627209984645,-13.6520626523353,
-12.6769153200256,-11.701767987716,-10.7266206554063,-10.1357873115492),
 .UNSPECIFIED.);
#525=B_SPLINE_CURVE_WITH_KNOTS('',3,(#18820,#18821,#18822,#18823,#18824,
#18825,#18826,#18827,#18828,#18829,#18830,#18831,#18832),.UNSPECIFIED.,
 .F.,.F.,(4,3,3,3,4),(-3.8526020043696,-2.92544199692899,-1.95029466461933,
-0.975147332309664,0.),.UNSPECIFIED.);
#526=B_SPLINE_CURVE_WITH_KNOTS('',3,(#18835,#18836,#18837,#18838,#18839,
#18840,#18841,#18842,#18843,#18844,#18845,#18846,#18847,#18848,#18849,#18850,
#18851,#18852,#18853),.UNSPECIFIED.,.F.,.F.,(4,3,3,3,3,3,4),(2.02057249175693,
2.925441996929,3.90058932923866,4.87573666154832,5.85088399385799,6.82603132616766,
7.59274844815668),.UNSPECIFIED.);
#527=B_SPLINE_CURVE_WITH_KNOTS('',3,(#18859,#18860,#18861,#18862,#18863,
#18864,#18865),.UNSPECIFIED.,.F.,.F.,(4,1,1,1,4),(40.8407044966673,41.1097812328693,
42.084928565179,43.0600758974886,44.0352232297983),.UNSPECIFIED.);
#528=B_SPLINE_CURVE_WITH_KNOTS('',3,(#18868,#18869,#18870,#18871,#18872,
#18873,#18874),.UNSPECIFIED.,.F.,.F.,(4,1,1,1,4),(40.8407044966673,41.7025254316425,
42.6776727639522,43.6528200962618,44.5576896014339),.UNSPECIFIED.);
#529=B_SPLINE_CURVE_WITH_KNOTS('',3,(#18879,#18880,#18881,#18882,#18883,
#18884,#18885,#18886,#18887,#18888),.UNSPECIFIED.,.F.,.F.,(4,1,1,1,1,1,
1,4),(34.5575191894877,35.2588972390113,36.234044571321,37.2091919036307,
38.1843392359403,39.15948656825,40.1346339005596,40.8407044966673),
 .UNSPECIFIED.);
#530=B_SPLINE_CURVE_WITH_KNOTS('',3,(#18889,#18890,#18891,#18892,#18893,
#18894,#18895,#18896,#18897,#18898,#18899),.UNSPECIFIED.,.F.,.F.,(4,1,1,
1,1,1,1,1,4),(34.5575191894877,34.8764941054748,35.8516414377845,36.8267887700942,
37.8019361024038,38.7770834347135,39.7522307670232,40.7273780993328,40.8407044966673),
 .UNSPECIFIED.);
#531=B_SPLINE_CURVE_WITH_KNOTS('',3,(#18904,#18905,#18906,#18907,#18908,
#18909,#18910,#18911,#18912,#18913,#18914),.UNSPECIFIED.,.F.,.F.,(4,1,1,
1,1,1,1,1,4),(28.2743338823081,28.4328659128437,29.4080132451533,30.383160577463,
31.3583079097727,32.3334552420823,33.308602574392,34.2837499067017,34.5575191894877),
 .UNSPECIFIED.);
#532=B_SPLINE_CURVE_WITH_KNOTS('',3,(#18915,#18916,#18917,#18918,#18919,
#18920,#18921,#18922,#18923,#18924),.UNSPECIFIED.,.F.,.F.,(4,1,1,1,1,1,
1,4),(28.2743338823081,29.0256101116168,30.0007574439265,30.9759047762362,
31.9510521085458,32.9261994408555,33.9013467731652,34.5575191894877),
 .UNSPECIFIED.);
#533=B_SPLINE_CURVE_WITH_KNOTS('',3,(#18929,#18930,#18931,#18932,#18933,
#18934,#18935,#18936,#18937,#18938),.UNSPECIFIED.,.F.,.F.,(4,1,1,1,1,1,
1,4),(21.9911485751285,22.5819819189857,23.5571292512954,24.532276583605,
25.5074239159147,26.4825712482243,27.457718580534,28.2743338823081),
 .UNSPECIFIED.);
#534=B_SPLINE_CURVE_WITH_KNOTS('',3,(#18939,#18940,#18941,#18942,#18943,
#18944,#18945,#18946,#18947,#18948,#18949),.UNSPECIFIED.,.F.,.F.,(4,1,1,
1,1,1,1,1,4),(21.9911485751285,22.1995787854492,23.1747261177589,24.1498734500685,
25.1250207823782,26.1001681146879,27.0753154469975,28.0504627793072,28.2743338823081),
 .UNSPECIFIED.);
#535=B_SPLINE_CURVE_WITH_KNOTS('',3,(#18955,#18956,#18957,#18958,#18959),
 .UNSPECIFIED.,.F.,.F.,(4,1,4),(14.3984001269719,15.3735474592815,15.7079632679489),
 .UNSPECIFIED.);
#536=B_SPLINE_CURVE_WITH_KNOTS('',3,(#18962,#18963,#18964,#18965,#18966),
 .UNSPECIFIED.,.F.,.F.,(4,1,4),(13.8759337553363,14.7808032605084,15.7079632679489),
 .UNSPECIFIED.);
#537=B_SPLINE_CURVE_WITH_KNOTS('',3,(#18968,#18969,#18970,#18971,#18972,
#18973,#18974,#18975,#18976,#18977,#18978),.UNSPECIFIED.,.F.,.F.,(4,1,1,
1,1,1,1,1,4),(15.7079632679489,15.755950592818,16.7310979251277,17.7062452574374,
18.681392589747,19.6565399220567,20.6316872543664,21.606834586676,21.9911485751285),
 .UNSPECIFIED.);
#538=B_SPLINE_CURVE_WITH_KNOTS('',3,(#18979,#18980,#18981,#18982,#18983,
#18984,#18985,#18986,#18987,#18988),.UNSPECIFIED.,.F.,.F.,(4,1,1,1,1,1,
1,4),(15.7079632679489,16.3486947915912,17.3238421239009,18.2989894562105,
19.2741367885202,20.2492841208299,21.2244314531395,21.9911485751285),
 .UNSPECIFIED.);
#539=B_SPLINE_CURVE_WITH_KNOTS('',3,(#19133,#19134,#19135,#19136,#19137,
#19138,#19139,#19140,#19141,#19142,#19143,#19144,#19145,#19146,#19147,#19148,
#19149,#19150,#19151,#19152,#19153,#19154,#19155,#19156,#19157,#19158,#19159,
#19160,#19161,#19162,#19163,#19164,#19165,#19166,#19167,#19168,#19169,#19170,
#19171,#19172,#19173,#19174,#19175,#19176,#19177,#19178,#19179,#19180,#19181),
 .UNSPECIFIED.,.F.,.F.,(4,3,3,3,3,3,3,3,3,3,3,3,3,3,3,3,4),(0.,0.0320333804888866,
0.0505515708593653,0.0603413132804416,0.0917900141854983,0.108096115778005,
0.122914675479851,0.145143248337739,0.168151513577436,0.177516949333476,
0.202471322707608,0.21794283081622,0.231200110368267,0.247503117401854,
0.263651632124391,0.277334442830003,0.286347380332244),.UNSPECIFIED.);
#540=B_SPLINE_CURVE_WITH_KNOTS('',3,(#19182,#19183,#19184,#19185,#19186,
#19187,#19188,#19189,#19190,#19191,#19192,#19193,#19194,#19195,#19196,#19197,
#19198,#19199,#19200,#19201,#19202,#19203,#19204,#19205,#19206,#19207,#19208,
#19209,#19210,#19211,#19212,#19213,#19214,#19215,#19216,#19217,#19218,#19219,
#19220,#19221,#19222,#19223,#19224,#19225,#19226,#19227,#19228,#19229,#19230),
 .UNSPECIFIED.,.F.,.F.,(4,3,3,3,3,3,3,3,3,3,3,3,3,3,3,3,4),(0.,0.0274305464075637,
0.0492901149097146,0.0591933555873536,0.0887250095166089,0.100015570674795,
0.108381796308415,0.130826479038955,0.152531076563578,0.162815893631175,
0.190691958353668,0.212372986031639,0.222945305605857,0.245534254906135,
0.257847836118801,0.274320152521146,0.28514280399515),.UNSPECIFIED.);
#541=B_SPLINE_CURVE_WITH_KNOTS('',3,(#19231,#19232,#19233,#19234,#19235,
#19236,#19237,#19238,#19239,#19240,#19241,#19242,#19243,#19244,#19245,#19246,
#19247,#19248,#19249,#19250,#19251,#19252,#19253,#19254,#19255),
 .UNSPECIFIED.,.F.,.F.,(4,3,3,3,3,3,3,3,4),(-10.1357873115492,-9.75147332309665,
-8.77632599078699,-7.80117865847732,-6.82603132616766,-5.85088399385799,
-4.87573666154833,-3.90058932923866,-3.8526020043696),.UNSPECIFIED.);
#542=B_SPLINE_CURVE_WITH_KNOTS('',3,(#19400,#19401,#19402,#19403,#19404,
#19405,#19406,#19407,#19408,#19409,#19410,#19411,#19412,#19413,#19414,#19415,
#19416,#19417,#19418,#19419,#19420,#19421,#19422,#19423,#19424,#19425,#19426,
#19427,#19428,#19429,#19430,#19431,#19432,#19433,#19434,#19435,#19436,#19437,
#19438,#19439,#19440,#19441,#19442,#19443,#19444,#19445,#19446,#19447,#19448),
 .UNSPECIFIED.,.F.,.F.,(4,3,3,3,3,3,3,3,3,3,3,3,3,3,3,3,4),(0.,0.0274305890506951,
0.0492901290331875,0.0591933603491513,0.0887250177779717,0.100015607166709,
0.108381835831352,0.13082647903896,0.152531071764912,0.162815892251191,
0.190691957318683,0.212372984486691,0.22294529735758,0.245534140364172,
0.257847701250626,0.274320152521159,0.285142803995162),.UNSPECIFIED.);
#543=B_SPLINE_CURVE_WITH_KNOTS('',3,(#19449,#19450,#19451,#19452,#19453,
#19454,#19455,#19456,#19457,#19458,#19459,#19460,#19461,#19462,#19463,#19464,
#19465,#19466,#19467,#19468,#19469,#19470,#19471,#19472,#19473),
 .UNSPECIFIED.,.F.,.F.,(4,3,3,3,3,3,3,3,4),(7.59274844815668,7.80117865847732,
8.77632599078698,9.75147332309665,10.7266206554063,11.701767987716,12.6769153200256,
13.6520626523353,13.8759337553363),.UNSPECIFIED.);
#544=B_SPLINE_CURVE_WITH_KNOTS('',3,(#19474,#19475,#19476,#19477,#19478,
#19479,#19480,#19481,#19482,#19483,#19484,#19485,#19486,#19487,#19488,#19489,
#19490,#19491,#19492,#19493,#19494,#19495,#19496,#19497,#19498,#19499,#19500,
#19501,#19502,#19503,#19504,#19505,#19506,#19507,#19508,#19509,#19510,#19511,
#19512,#19513,#19514,#19515,#19516,#19517,#19518,#19519,#19520,#19521,#19522),
 .UNSPECIFIED.,.F.,.F.,(4,3,3,3,3,3,3,3,3,3,3,3,3,3,3,3,4),(0.,0.0320334058164849,
0.0505515938322513,0.0603413311462071,0.0917900214840119,0.108096111687201,
0.122914678304232,0.145143248337743,0.168151527562726,0.177516955081398,
0.202471327018552,0.217942288122009,0.231200024743484,0.24750284136614,
0.263651600306541,0.277334442830014,0.286347380332252),.UNSPECIFIED.);
#553=SHAPE_REPRESENTATION_RELATIONSHIP('SRR','None',#19673,#563);
#563=ADVANCED_BREP_SHAPE_REPRESENTATION('',(#583),#19616);
#573=STYLED_ITEM('',(#19733),#583);
#583=MANIFOLD_SOLID_BREP('Body1',#7111);
#656=FACE_BOUND('',#1682,.T.);
#657=FACE_BOUND('',#1691,.T.);
#811=PLANE('',#7735);
#812=PLANE('',#7737);
#813=PLANE('',#7738);
#814=PLANE('',#7739);
#815=PLANE('',#7740);
#816=PLANE('',#7741);
#817=PLANE('',#7742);
#818=PLANE('',#7743);
#1198=FACE_OUTER_BOUND('',#1668,.T.);
#1199=FACE_OUTER_BOUND('',#1669,.T.);
#1200=FACE_OUTER_BOUND('',#1670,.T.);
#1201=FACE_OUTER_BOUND('',#1671,.T.);
#1202=FACE_OUTER_BOUND('',#1672,.T.);
#1203=FACE_OUTER_BOUND('',#1673,.T.);
#1204=FACE_OUTER_BOUND('',#1674,.T.);
#1205=FACE_OUTER_BOUND('',#1675,.T.);
#1206=FACE_OUTER_BOUND('',#1676,.T.);
#1207=FACE_OUTER_BOUND('',#1677,.T.);
#1208=FACE_OUTER_BOUND('',#1678,.T.);
#1209=FACE_OUTER_BOUND('',#1679,.T.);
#1210=FACE_OUTER_BOUND('',#1680,.T.);
#1211=FACE_OUTER_BOUND('',#1681,.T.);
#1212=FACE_OUTER_BOUND('',#1683,.T.);
#1213=FACE_OUTER_BOUND('',#1684,.T.);
#1214=FACE_OUTER_BOUND('',#1685,.T.);
#1215=FACE_OUTER_BOUND('',#1686,.T.);
#1216=FACE_OUTER_BOUND('',#1687,.T.);
#1217=FACE_OUTER_BOUND('',#1688,.T.);
#1218=FACE_OUTER_BOUND('',#1689,.T.);
#1219=FACE_OUTER_BOUND('',#1690,.T.);
#1668=EDGE_LOOP('',(#6426,#6427,#6428));
#1669=EDGE_LOOP('',(#6429,#6430,#6431,#6432,#6433));
#1670=EDGE_LOOP('',(#6434,#6435,#6436,#6437));
#1671=EDGE_LOOP('',(#6438,#6439,#6440,#6441));
#1672=EDGE_LOOP('',(#6442,#6443,#6444,#6445));
#1673=EDGE_LOOP('',(#6446,#6447,#6448,#6449));
#1674=EDGE_LOOP('',(#6450,#6451,#6452,#6453));
#1675=EDGE_LOOP('',(#6454,#6455,#6456,#6457));
#1676=EDGE_LOOP('',(#6458,#6459,#6460,#6461));
#1677=EDGE_LOOP('',(#6462,#6463,#6464,#6465));
#1678=EDGE_LOOP('',(#6466,#6467,#6468,#6469));
#1679=EDGE_LOOP('',(#6470,#6471,#6472,#6473,#6474,#6475,#6476,#6477,#6478,
#6479,#6480,#6481,#6482,#6483));
#1680=EDGE_LOOP('',(#6484,#6485,#6486,#6487,#6488,#6489,#6490,#6491,#6492,
#6493,#6494,#6495,#6496));
#1681=EDGE_LOOP('',(#6497,#6498,#6499,#6500,#6501,#6502));
#1682=EDGE_LOOP('',(#6503,#6504,#6505,#6506));
#1683=EDGE_LOOP('',(#6507,#6508,#6509,#6510));
#1684=EDGE_LOOP('',(#6511,#6512,#6513,#6514));
#1685=EDGE_LOOP('',(#6515,#6516,#6517,#6518));
#1686=EDGE_LOOP('',(#6519,#6520,#6521,#6522));
#1687=EDGE_LOOP('',(#6523,#6524,#6525,#6526));
#1688=EDGE_LOOP('',(#6527,#6528,#6529,#6530));
#1689=EDGE_LOOP('',(#6531,#6532,#6533,#6534));
#1690=EDGE_LOOP('',(#6535,#6536,#6537,#6538,#6539,#6540));
#1691=EDGE_LOOP('',(#6541,#6542,#6543,#6544,#6545));
#2127=LINE('',#18656,#2586);
#2128=LINE('',#18669,#2587);
#2129=LINE('',#18716,#2588);
#2130=LINE('',#18770,#2589);
#2131=LINE('',#18818,#2590);
#2132=LINE('',#18857,#2591);
#2133=LINE('',#18878,#2592);
#2134=LINE('',#18903,#2593);
#2135=LINE('',#18928,#2594);
#2136=LINE('',#18953,#2595);
#2137=LINE('',#19526,#2596);
#2138=LINE('',#19528,#2597);
#2139=LINE('',#19530,#2598);
#2140=LINE('',#19532,#2599);
#2141=LINE('',#19534,#2600);
#2142=LINE('',#19535,#2601);
#2143=LINE('',#19540,#2602);
#2144=LINE('',#19541,#2603);
#2145=LINE('',#19542,#2604);
#2146=LINE('',#19545,#2605);
#2147=LINE('',#19546,#2606);
#2148=LINE('',#19549,#2607);
#2149=LINE('',#19550,#2608);
#2150=LINE('',#19553,#2609);
#2151=LINE('',#19554,#2610);
#2152=LINE('',#19557,#2611);
#2153=LINE('',#19558,#2612);
#2154=LINE('',#19560,#2613);
#2586=VECTOR('',#9190,0.15);
#2587=VECTOR('',#9195,0.15);
#2588=VECTOR('',#9200,0.15);
#2589=VECTOR('',#9203,0.15);
#2590=VECTOR('',#9206,0.15);
#2591=VECTOR('',#9211,0.1543);
#2592=VECTOR('',#9216,0.1543);
#2593=VECTOR('',#9219,0.1543);
#2594=VECTOR('',#9222,0.1543);
#2595=VECTOR('',#9225,0.1543);
#2596=VECTOR('',#9232,1.);
#2597=VECTOR('',#9233,1.);
#2598=VECTOR('',#9234,1.);
#2599=VECTOR('',#9235,1.);
#2600=VECTOR('',#9236,1.);
#2601=VECTOR('',#9237,1.);
#2602=VECTOR('',#9242,1.);
#2603=VECTOR('',#9243,1.);
#2604=VECTOR('',#9244,1.);
#2605=VECTOR('',#9247,1.);
#2606=VECTOR('',#9248,1.);
#2607=VECTOR('',#9251,1.);
#2608=VECTOR('',#9252,1.);
#2609=VECTOR('',#9255,1.);
#2610=VECTOR('',#9256,1.);
#2611=VECTOR('',#9259,1.);
#2612=VECTOR('',#9260,1.);
#2613=VECTOR('',#9263,1.);
#2801=CIRCLE('',#7720,0.12645);
#2802=CIRCLE('',#7722,0.12645);
#2803=CIRCLE('',#7726,0.12645);
#2804=CIRCLE('',#7728,0.1543);
#2805=CIRCLE('',#7733,0.1543);
#3433=VERTEX_POINT('',#18654);
#3434=VERTEX_POINT('',#18655);
#3435=VERTEX_POINT('',#18657);
#3436=VERTEX_POINT('',#18667);
#3437=VERTEX_POINT('',#18668);
#3438=VERTEX_POINT('',#18670);
#3439=VERTEX_POINT('',#18714);
#3440=VERTEX_POINT('',#18715);
#3441=VERTEX_POINT('',#18768);
#3442=VERTEX_POINT('',#18769);
#3443=VERTEX_POINT('',#18816);
#3444=VERTEX_POINT('',#18817);
#3445=VERTEX_POINT('',#18819);
#3446=VERTEX_POINT('',#18833);
#3447=VERTEX_POINT('',#18855);
#3448=VERTEX_POINT('',#18856);
#3449=VERTEX_POINT('',#18858);
#3450=VERTEX_POINT('',#18866);
#3451=VERTEX_POINT('',#18876);
#3452=VERTEX_POINT('',#18877);
#3453=VERTEX_POINT('',#18901);
#3454=VERTEX_POINT('',#18902);
#3455=VERTEX_POINT('',#18926);
#3456=VERTEX_POINT('',#18927);
#3457=VERTEX_POINT('',#18951);
#3458=VERTEX_POINT('',#18952);
#3459=VERTEX_POINT('',#18954);
#3460=VERTEX_POINT('',#18960);
#3461=VERTEX_POINT('',#19524);
#3462=VERTEX_POINT('',#19525);
#3463=VERTEX_POINT('',#19527);
#3464=VERTEX_POINT('',#19529);
#3465=VERTEX_POINT('',#19531);
#3466=VERTEX_POINT('',#19533);
#3467=VERTEX_POINT('',#19538);
#3468=VERTEX_POINT('',#19539);
#3469=VERTEX_POINT('',#19544);
#3470=VERTEX_POINT('',#19548);
#3471=VERTEX_POINT('',#19552);
#3472=VERTEX_POINT('',#19556);
#4438=EDGE_CURVE('',#3433,#3434,#2127,.T.);
#4439=EDGE_CURVE('',#3435,#3434,#2801,.F.);
#4440=EDGE_CURVE('',#3435,#3433,#518,.T.);
#4441=EDGE_CURVE('',#3436,#3437,#2128,.T.);
#4442=EDGE_CURVE('',#3437,#3438,#519,.T.);
#4443=EDGE_CURVE('',#3434,#3438,#2802,.F.);
#4444=EDGE_CURVE('',#3433,#3436,#520,.T.);
#4445=EDGE_CURVE('',#3439,#3440,#2129,.T.);
#4446=EDGE_CURVE('',#3440,#3437,#521,.T.);
#4447=EDGE_CURVE('',#3436,#3439,#522,.T.);
#4448=EDGE_CURVE('',#3441,#3442,#2130,.T.);
#4449=EDGE_CURVE('',#3442,#3440,#523,.T.);
#4450=EDGE_CURVE('',#3439,#3441,#524,.T.);
#4451=EDGE_CURVE('',#3443,#3444,#2131,.T.);
#4452=EDGE_CURVE('',#3443,#3445,#525,.T.);
#4453=EDGE_CURVE('',#3446,#3445,#2803,.T.);
#4454=EDGE_CURVE('',#3446,#3444,#526,.T.);
#4455=EDGE_CURVE('',#3447,#3448,#2132,.T.);
#4456=EDGE_CURVE('',#3448,#3449,#527,.T.);
#4457=EDGE_CURVE('',#3450,#3449,#2804,.T.);
#4458=EDGE_CURVE('',#3447,#3450,#528,.T.);
#4459=EDGE_CURVE('',#3451,#3452,#2133,.T.);
#4460=EDGE_CURVE('',#3452,#3448,#529,.T.);
#4461=EDGE_CURVE('',#3451,#3447,#530,.T.);
#4462=EDGE_CURVE('',#3453,#3454,#2134,.T.);
#4463=EDGE_CURVE('',#3454,#3452,#531,.T.);
#4464=EDGE_CURVE('',#3453,#3451,#532,.T.);
#4465=EDGE_CURVE('',#3455,#3456,#2135,.T.);
#4466=EDGE_CURVE('',#3456,#3454,#533,.T.);
#4467=EDGE_CURVE('',#3455,#3453,#534,.T.);
#4468=EDGE_CURVE('',#3457,#3458,#2136,.T.);
#4469=EDGE_CURVE('',#3459,#3457,#535,.T.);
#4470=EDGE_CURVE('',#3460,#3459,#2805,.T.);
#4471=EDGE_CURVE('',#3460,#3458,#536,.T.);
#4472=EDGE_CURVE('',#3458,#3456,#537,.T.);
#4473=EDGE_CURVE('',#3457,#3455,#538,.T.);
#4474=EDGE_CURVE('',#3449,#3435,#539,.T.);
#4475=EDGE_CURVE('',#3445,#3460,#540,.T.);
#4476=EDGE_CURVE('',#3441,#3443,#541,.T.);
#4477=EDGE_CURVE('',#3438,#3450,#542,.T.);
#4478=EDGE_CURVE('',#3444,#3442,#543,.T.);
#4479=EDGE_CURVE('',#3459,#3446,#544,.T.);
#4480=EDGE_CURVE('',#3461,#3462,#2137,.T.);
#4481=EDGE_CURVE('',#3462,#3463,#2138,.T.);
#4482=EDGE_CURVE('',#3463,#3464,#2139,.T.);
#4483=EDGE_CURVE('',#3464,#3465,#2140,.T.);
#4484=EDGE_CURVE('',#3465,#3466,#2141,.T.);
#4485=EDGE_CURVE('',#3466,#3461,#2142,.T.);
#4486=EDGE_CURVE('',#3467,#3468,#2143,.T.);
#4487=EDGE_CURVE('',#3468,#3461,#2144,.T.);
#4488=EDGE_CURVE('',#3467,#3466,#2145,.T.);
#4489=EDGE_CURVE('',#3469,#3467,#2146,.T.);
#4490=EDGE_CURVE('',#3469,#3465,#2147,.T.);
#4491=EDGE_CURVE('',#3470,#3469,#2148,.T.);
#4492=EDGE_CURVE('',#3470,#3464,#2149,.T.);
#4493=EDGE_CURVE('',#3471,#3470,#2150,.T.);
#4494=EDGE_CURVE('',#3471,#3463,#2151,.T.);
#4495=EDGE_CURVE('',#3472,#3471,#2152,.T.);
#4496=EDGE_CURVE('',#3472,#3462,#2153,.T.);
#4497=EDGE_CURVE('',#3468,#3472,#2154,.T.);
#6426=ORIENTED_EDGE('',*,*,#4438,.T.);
#6427=ORIENTED_EDGE('',*,*,#4439,.F.);
#6428=ORIENTED_EDGE('',*,*,#4440,.T.);
#6429=ORIENTED_EDGE('',*,*,#4441,.T.);
#6430=ORIENTED_EDGE('',*,*,#4442,.T.);
#6431=ORIENTED_EDGE('',*,*,#4443,.F.);
#6432=ORIENTED_EDGE('',*,*,#4438,.F.);
#6433=ORIENTED_EDGE('',*,*,#4444,.T.);
#6434=ORIENTED_EDGE('',*,*,#4445,.T.);
#6435=ORIENTED_EDGE('',*,*,#4446,.T.);
#6436=ORIENTED_EDGE('',*,*,#4441,.F.);
#6437=ORIENTED_EDGE('',*,*,#4447,.T.);
#6438=ORIENTED_EDGE('',*,*,#4448,.T.);
#6439=ORIENTED_EDGE('',*,*,#4449,.T.);
#6440=ORIENTED_EDGE('',*,*,#4445,.F.);
#6441=ORIENTED_EDGE('',*,*,#4450,.T.);
#6442=ORIENTED_EDGE('',*,*,#4451,.F.);
#6443=ORIENTED_EDGE('',*,*,#4452,.T.);
#6444=ORIENTED_EDGE('',*,*,#4453,.F.);
#6445=ORIENTED_EDGE('',*,*,#4454,.T.);
#6446=ORIENTED_EDGE('',*,*,#4455,.T.);
#6447=ORIENTED_EDGE('',*,*,#4456,.T.);
#6448=ORIENTED_EDGE('',*,*,#4457,.F.);
#6449=ORIENTED_EDGE('',*,*,#4458,.F.);
#6450=ORIENTED_EDGE('',*,*,#4459,.T.);
#6451=ORIENTED_EDGE('',*,*,#4460,.T.);
#6452=ORIENTED_EDGE('',*,*,#4455,.F.);
#6453=ORIENTED_EDGE('',*,*,#4461,.F.);
#6454=ORIENTED_EDGE('',*,*,#4462,.T.);
#6455=ORIENTED_EDGE('',*,*,#4463,.T.);
#6456=ORIENTED_EDGE('',*,*,#4459,.F.);
#6457=ORIENTED_EDGE('',*,*,#4464,.F.);
#6458=ORIENTED_EDGE('',*,*,#4465,.T.);
#6459=ORIENTED_EDGE('',*,*,#4466,.T.);
#6460=ORIENTED_EDGE('',*,*,#4462,.F.);
#6461=ORIENTED_EDGE('',*,*,#4467,.F.);
#6462=ORIENTED_EDGE('',*,*,#4468,.F.);
#6463=ORIENTED_EDGE('',*,*,#4469,.F.);
#6464=ORIENTED_EDGE('',*,*,#4470,.F.);
#6465=ORIENTED_EDGE('',*,*,#4471,.T.);
#6466=ORIENTED_EDGE('',*,*,#4468,.T.);
#6467=ORIENTED_EDGE('',*,*,#4472,.T.);
#6468=ORIENTED_EDGE('',*,*,#4465,.F.);
#6469=ORIENTED_EDGE('',*,*,#4473,.F.);
#6470=ORIENTED_EDGE('',*,*,#4474,.F.);
#6471=ORIENTED_EDGE('',*,*,#4456,.F.);
#6472=ORIENTED_EDGE('',*,*,#4460,.F.);
#6473=ORIENTED_EDGE('',*,*,#4463,.F.);
#6474=ORIENTED_EDGE('',*,*,#4466,.F.);
#6475=ORIENTED_EDGE('',*,*,#4472,.F.);
#6476=ORIENTED_EDGE('',*,*,#4471,.F.);
#6477=ORIENTED_EDGE('',*,*,#4475,.F.);
#6478=ORIENTED_EDGE('',*,*,#4452,.F.);
#6479=ORIENTED_EDGE('',*,*,#4476,.F.);
#6480=ORIENTED_EDGE('',*,*,#4450,.F.);
#6481=ORIENTED_EDGE('',*,*,#4447,.F.);
#6482=ORIENTED_EDGE('',*,*,#4444,.F.);
#6483=ORIENTED_EDGE('',*,*,#4440,.F.);
#6484=ORIENTED_EDGE('',*,*,#4477,.F.);
#6485=ORIENTED_EDGE('',*,*,#4442,.F.);
#6486=ORIENTED_EDGE('',*,*,#4446,.F.);
#6487=ORIENTED_EDGE('',*,*,#4449,.F.);
#6488=ORIENTED_EDGE('',*,*,#4478,.F.);
#6489=ORIENTED_EDGE('',*,*,#4454,.F.);
#6490=ORIENTED_EDGE('',*,*,#4479,.F.);
#6491=ORIENTED_EDGE('',*,*,#4469,.T.);
#6492=ORIENTED_EDGE('',*,*,#4473,.T.);
#6493=ORIENTED_EDGE('',*,*,#4467,.T.);
#6494=ORIENTED_EDGE('',*,*,#4464,.T.);
#6495=ORIENTED_EDGE('',*,*,#4461,.T.);
#6496=ORIENTED_EDGE('',*,*,#4458,.T.);
#6497=ORIENTED_EDGE('',*,*,#4480,.T.);
#6498=ORIENTED_EDGE('',*,*,#4481,.T.);
#6499=ORIENTED_EDGE('',*,*,#4482,.T.);
#6500=ORIENTED_EDGE('',*,*,#4483,.T.);
#6501=ORIENTED_EDGE('',*,*,#4484,.T.);
#6502=ORIENTED_EDGE('',*,*,#4485,.T.);
#6503=ORIENTED_EDGE('',*,*,#4475,.T.);
#6504=ORIENTED_EDGE('',*,*,#4470,.T.);
#6505=ORIENTED_EDGE('',*,*,#4479,.T.);
#6506=ORIENTED_EDGE('',*,*,#4453,.T.);
#6507=ORIENTED_EDGE('',*,*,#4451,.T.);
#6508=ORIENTED_EDGE('',*,*,#4478,.T.);
#6509=ORIENTED_EDGE('',*,*,#4448,.F.);
#6510=ORIENTED_EDGE('',*,*,#4476,.T.);
#6511=ORIENTED_EDGE('',*,*,#4486,.T.);
#6512=ORIENTED_EDGE('',*,*,#4487,.T.);
#6513=ORIENTED_EDGE('',*,*,#4485,.F.);
#6514=ORIENTED_EDGE('',*,*,#4488,.F.);
#6515=ORIENTED_EDGE('',*,*,#4489,.T.);
#6516=ORIENTED_EDGE('',*,*,#4488,.T.);
#6517=ORIENTED_EDGE('',*,*,#4484,.F.);
#6518=ORIENTED_EDGE('',*,*,#4490,.F.);
#6519=ORIENTED_EDGE('',*,*,#4491,.T.);
#6520=ORIENTED_EDGE('',*,*,#4490,.T.);
#6521=ORIENTED_EDGE('',*,*,#4483,.F.);
#6522=ORIENTED_EDGE('',*,*,#4492,.F.);
#6523=ORIENTED_EDGE('',*,*,#4493,.T.);
#6524=ORIENTED_EDGE('',*,*,#4492,.T.);
#6525=ORIENTED_EDGE('',*,*,#4482,.F.);
#6526=ORIENTED_EDGE('',*,*,#4494,.F.);
#6527=ORIENTED_EDGE('',*,*,#4495,.T.);
#6528=ORIENTED_EDGE('',*,*,#4494,.T.);
#6529=ORIENTED_EDGE('',*,*,#4481,.F.);
#6530=ORIENTED_EDGE('',*,*,#4496,.F.);
#6531=ORIENTED_EDGE('',*,*,#4497,.T.);
#6532=ORIENTED_EDGE('',*,*,#4496,.T.);
#6533=ORIENTED_EDGE('',*,*,#4480,.F.);
#6534=ORIENTED_EDGE('',*,*,#4487,.F.);
#6535=ORIENTED_EDGE('',*,*,#4497,.F.);
#6536=ORIENTED_EDGE('',*,*,#4486,.F.);
#6537=ORIENTED_EDGE('',*,*,#4489,.F.);
#6538=ORIENTED_EDGE('',*,*,#4491,.F.);
#6539=ORIENTED_EDGE('',*,*,#4493,.F.);
#6540=ORIENTED_EDGE('',*,*,#4495,.F.);
#6541=ORIENTED_EDGE('',*,*,#4474,.T.);
#6542=ORIENTED_EDGE('',*,*,#4439,.T.);
#6543=ORIENTED_EDGE('',*,*,#4443,.T.);
#6544=ORIENTED_EDGE('',*,*,#4477,.T.);
#6545=ORIENTED_EDGE('',*,*,#4457,.T.);
#6686=CYLINDRICAL_SURFACE('',#7719,0.12645);
#6687=CYLINDRICAL_SURFACE('',#7721,0.12645);
#6688=CYLINDRICAL_SURFACE('',#7723,0.12645);
#6689=CYLINDRICAL_SURFACE('',#7724,0.12645);
#6690=CYLINDRICAL_SURFACE('',#7725,0.12645);
#6691=CYLINDRICAL_SURFACE('',#7727,0.1543);
#6692=CYLINDRICAL_SURFACE('',#7729,0.1543);
#6693=CYLINDRICAL_SURFACE('',#7730,0.1543);
#6694=CYLINDRICAL_SURFACE('',#7731,0.1543);
#6695=CYLINDRICAL_SURFACE('',#7732,0.1543);
#6696=CYLINDRICAL_SURFACE('',#7734,0.1543);
#6697=CYLINDRICAL_SURFACE('',#7736,0.12645);
#7077=ADVANCED_FACE('',(#1198),#6686,.F.);
#7078=ADVANCED_FACE('',(#1199),#6687,.F.);
#7079=ADVANCED_FACE('',(#1200),#6688,.F.);
#7080=ADVANCED_FACE('',(#1201),#6689,.F.);
#7081=ADVANCED_FACE('',(#1202),#6690,.F.);
#7082=ADVANCED_FACE('',(#1203),#6691,.F.);
#7083=ADVANCED_FACE('',(#1204),#6692,.F.);
#7084=ADVANCED_FACE('',(#1205),#6693,.F.);
#7085=ADVANCED_FACE('',(#1206),#6694,.F.);
#7086=ADVANCED_FACE('',(#1207),#6695,.F.);
#7087=ADVANCED_FACE('',(#1208),#6696,.F.);
#7088=ADVANCED_FACE('',(#1209),#169,.F.);
#7089=ADVANCED_FACE('',(#1210),#170,.F.);
#7090=ADVANCED_FACE('',(#1211,#656),#811,.T.);
#7091=ADVANCED_FACE('',(#1212),#6697,.F.);
#7092=ADVANCED_FACE('',(#1213),#812,.T.);
#7093=ADVANCED_FACE('',(#1214),#813,.T.);
#7094=ADVANCED_FACE('',(#1215),#814,.T.);
#7095=ADVANCED_FACE('',(#1216),#815,.T.);
#7096=ADVANCED_FACE('',(#1217),#816,.T.);
#7097=ADVANCED_FACE('',(#1218),#817,.T.);
#7098=ADVANCED_FACE('',(#1219,#657),#818,.F.);
#7111=CLOSED_SHELL('',(#7077,#7078,#7079,#7080,#7081,#7082,#7083,#7084,
#7085,#7086,#7087,#7088,#7089,#7090,#7091,#7092,#7093,#7094,#7095,#7096,
#7097,#7098));
#7718=AXIS2_PLACEMENT_3D('',#18652,#9186,#9187);
#7719=AXIS2_PLACEMENT_3D('',#18653,#9188,#9189);
#7720=AXIS2_PLACEMENT_3D('',#18658,#9191,#9192);
#7721=AXIS2_PLACEMENT_3D('',#18666,#9193,#9194);
#7722=AXIS2_PLACEMENT_3D('',#18690,#9196,#9197);
#7723=AXIS2_PLACEMENT_3D('',#18713,#9198,#9199);
#7724=AXIS2_PLACEMENT_3D('',#18767,#9201,#9202);
#7725=AXIS2_PLACEMENT_3D('',#18815,#9204,#9205);
#7726=AXIS2_PLACEMENT_3D('',#18834,#9207,#9208);
#7727=AXIS2_PLACEMENT_3D('',#18854,#9209,#9210);
#7728=AXIS2_PLACEMENT_3D('',#18867,#9212,#9213);
#7729=AXIS2_PLACEMENT_3D('',#18875,#9214,#9215);
#7730=AXIS2_PLACEMENT_3D('',#18900,#9217,#9218);
#7731=AXIS2_PLACEMENT_3D('',#18925,#9220,#9221);
#7732=AXIS2_PLACEMENT_3D('',#18950,#9223,#9224);
#7733=AXIS2_PLACEMENT_3D('',#18961,#9226,#9227);
#7734=AXIS2_PLACEMENT_3D('',#18967,#9228,#9229);
#7735=AXIS2_PLACEMENT_3D('',#19523,#9230,#9231);
#7736=AXIS2_PLACEMENT_3D('',#19536,#9238,#9239);
#7737=AXIS2_PLACEMENT_3D('',#19537,#9240,#9241);
#7738=AXIS2_PLACEMENT_3D('',#19543,#9245,#9246);
#7739=AXIS2_PLACEMENT_3D('',#19547,#9249,#9250);
#7740=AXIS2_PLACEMENT_3D('',#19551,#9253,#9254);
#7741=AXIS2_PLACEMENT_3D('',#19555,#9257,#9258);
#7742=AXIS2_PLACEMENT_3D('',#19559,#9261,#9262);
#7743=AXIS2_PLACEMENT_3D('',#19561,#9264,#9265);
#9186=DIRECTION('axis',(0.,0.,1.));
#9187=DIRECTION('refdir',(1.,0.,0.));
#9188=DIRECTION('center_axis',(0.,0.,-1.));
#9189=DIRECTION('ref_axis',(1.,0.,0.));
#9190=DIRECTION('',(0.,0.,-1.));
#9191=DIRECTION('center_axis',(0.,0.,-1.));
#9192=DIRECTION('ref_axis',(1.,0.,0.));
#9193=DIRECTION('center_axis',(0.,0.,-1.));
#9194=DIRECTION('ref_axis',(1.,0.,0.));
#9195=DIRECTION('',(0.,0.,-1.));
#9196=DIRECTION('center_axis',(0.,0.,-1.));
#9197=DIRECTION('ref_axis',(1.,0.,0.));
#9198=DIRECTION('center_axis',(0.,0.,-1.));
#9199=DIRECTION('ref_axis',(1.,0.,0.));
#9200=DIRECTION('',(0.,0.,-1.));
#9201=DIRECTION('center_axis',(0.,0.,-1.));
#9202=DIRECTION('ref_axis',(1.,0.,0.));
#9203=DIRECTION('',(0.,0.,-1.));
#9204=DIRECTION('center_axis',(0.,0.,-1.));
#9205=DIRECTION('ref_axis',(0.937385399639056,-0.348293859468591,0.));
#9206=DIRECTION('',(0.,0.,-1.));
#9207=DIRECTION('center_axis',(0.,0.,-1.));
#9208=DIRECTION('ref_axis',(1.,0.,0.));
#9209=DIRECTION('center_axis',(0.,0.,-1.));
#9210=DIRECTION('ref_axis',(0.28361887368566,0.958937085782627,0.));
#9211=DIRECTION('',(1.22464679914735E-16,8.07419868282478E-31,-1.));
#9212=DIRECTION('center_axis',(0.,0.,1.));
#9213=DIRECTION('ref_axis',(1.,6.71554824363804E-15,0.));
#9214=DIRECTION('center_axis',(0.,0.,-1.));
#9215=DIRECTION('ref_axis',(1.,6.71554824363804E-15,0.));
#9216=DIRECTION('',(1.22464679914735E-16,8.07419868282478E-31,-1.));
#9217=DIRECTION('center_axis',(0.,0.,-1.));
#9218=DIRECTION('ref_axis',(1.,6.71554824363804E-15,0.));
#9219=DIRECTION('',(1.22464679914735E-16,8.07419868282478E-31,-1.));
#9220=DIRECTION('center_axis',(0.,0.,-1.));
#9221=DIRECTION('ref_axis',(1.,6.71554824363804E-15,0.));
#9222=DIRECTION('',(1.22464679914735E-16,8.07419868282478E-31,-1.));
#9223=DIRECTION('center_axis',(0.,0.,-1.));
#9224=DIRECTION('ref_axis',(-0.60895050335979,-0.793208222636313,0.));
#9225=DIRECTION('',(1.22464679914735E-16,8.07419868282478E-31,-1.));
#9226=DIRECTION('center_axis',(0.,0.,-1.));
#9227=DIRECTION('ref_axis',(1.,6.71554824363804E-15,0.));
#9228=DIRECTION('center_axis',(0.,0.,-1.));
#9229=DIRECTION('ref_axis',(1.,6.71554824363804E-15,0.));
#9230=DIRECTION('center_axis',(0.,0.,1.));
#9231=DIRECTION('ref_axis',(1.,0.,0.));
#9232=DIRECTION('',(0.5,0.866025403784439,0.));
#9233=DIRECTION('',(-0.5,0.866025403784439,0.));
#9234=DIRECTION('',(-1.,0.,0.));
#9235=DIRECTION('',(-0.5,-0.866025403784439,0.));
#9236=DIRECTION('',(0.5,-0.866025403784439,0.));
#9237=DIRECTION('',(1.,-3.49629579342466E-16,0.));
#9238=DIRECTION('center_axis',(0.,0.,-1.));
#9239=DIRECTION('ref_axis',(1.,0.,0.));
#9240=DIRECTION('center_axis',(-3.49629579342466E-16,-1.,0.));
#9241=DIRECTION('ref_axis',(1.,-3.49629579342466E-16,0.));
#9242=DIRECTION('',(1.,-3.49629579342466E-16,0.));
#9243=DIRECTION('',(0.,0.,1.));
#9244=DIRECTION('',(0.,0.,1.));
#9245=DIRECTION('center_axis',(-0.866025403784439,-0.5,0.));
#9246=DIRECTION('ref_axis',(0.5,-0.866025403784439,0.));
#9247=DIRECTION('',(0.5,-0.866025403784439,0.));
#9248=DIRECTION('',(0.,0.,1.));
#9249=DIRECTION('center_axis',(-0.866025403784439,0.5,0.));
#9250=DIRECTION('ref_axis',(-0.5,-0.866025403784439,0.));
#9251=DIRECTION('',(-0.5,-0.866025403784439,0.));
#9252=DIRECTION('',(0.,0.,1.));
#9253=DIRECTION('center_axis',(0.,1.,0.));
#9254=DIRECTION('ref_axis',(-1.,0.,0.));
#9255=DIRECTION('',(-1.,0.,0.));
#9256=DIRECTION('',(0.,0.,1.));
#9257=DIRECTION('center_axis',(0.866025403784439,0.5,0.));
#9258=DIRECTION('ref_axis',(-0.5,0.866025403784439,0.));
#9259=DIRECTION('',(-0.5,0.866025403784439,0.));
#9260=DIRECTION('',(0.,0.,1.));
#9261=DIRECTION('center_axis',(0.866025403784439,-0.5,0.));
#9262=DIRECTION('ref_axis',(0.5,0.866025403784439,0.));
#9263=DIRECTION('',(0.5,0.866025403784439,0.));
#9264=DIRECTION('center_axis',(0.,0.,1.));
#9265=DIRECTION('ref_axis',(1.,0.,0.));
#18652=CARTESIAN_POINT('',(0.,0.,0.));
#18653=CARTESIAN_POINT('Origin',(0.,0.,0.12));
#18654=CARTESIAN_POINT('',(-0.12639138516214,8.91322620741042E-5,0.00934196736194174));
#18655=CARTESIAN_POINT('',(-0.12645,1.54856587752183E-17,-5.55111512312578E-17));
#18656=CARTESIAN_POINT('',(-0.12645,1.54856587752183E-17,0.12));
#18657=CARTESIAN_POINT('',(-0.0488748409397564,0.116622692573588,0.));
#18658=CARTESIAN_POINT('Origin',(0.,0.,0.));
#18659=CARTESIAN_POINT('Ctrl Pts',(-0.0489111879062984,0.116810626195002,
1.20007714660797E-17));
#18660=CARTESIAN_POINT('Ctrl Pts',(-0.0838963038512042,0.101957324585112,
0.00240024091002088));
#18661=CARTESIAN_POINT('Ctrl Pts',(-0.11198221847721,0.0702793053867637,
0.00480048182004174));
#18662=CARTESIAN_POINT('Ctrl Pts',(-0.122072221370749,0.0336561163696377,
0.00720072273006261));
#18663=CARTESIAN_POINT('Ctrl Pts',(-0.125072637487486,0.022765653033531,
0.00791447094068899));
#18664=CARTESIAN_POINT('Ctrl Pts',(-0.126481745582665,0.0114379076904012,
0.00862821915131536));
#18665=CARTESIAN_POINT('Ctrl Pts',(-0.12639138516214,8.91322620741042E-5,
0.00934196736194174));
#18666=CARTESIAN_POINT('Origin',(0.,0.,0.12));
#18667=CARTESIAN_POINT('',(-0.126396145829628,-9.95859796292312E-5,0.0593419673619417));
#18668=CARTESIAN_POINT('',(-0.126575671592806,-7.20628672610732E-5,0.0456580326380584));
#18669=CARTESIAN_POINT('',(-0.12645,1.54856587752183E-17,0.12));
#18670=CARTESIAN_POINT('',(-0.10808967569503,-0.0656218295092665,0.));
#18671=CARTESIAN_POINT('Ctrl Pts',(-0.126575671592806,-7.20628672610732E-5,
0.0456580326380584));
#18672=CARTESIAN_POINT('Ctrl Pts',(-0.126327459688109,0.0361497101693465,
0.0433719816070355));
#18673=CARTESIAN_POINT('Ctrl Pts',(-0.109912066394173,0.0725710138228805,
0.0410859305760125));
#18674=CARTESIAN_POINT('Ctrl Pts',(-0.0824515099939393,0.0961223418729112,
0.0387998795449896));
#18675=CARTESIAN_POINT('Ctrl Pts',(-0.05137998778939,0.122770586059505,
0.036213220908657));
#18676=CARTESIAN_POINT('Ctrl Pts',(-0.00616751748104999,0.132941603485868,
0.0336265622723243));
#18677=CARTESIAN_POINT('Ctrl Pts',(0.0333172074018229,0.122176268745047,
0.0310399036359917));
#18678=CARTESIAN_POINT('Ctrl Pts',(0.0728019322846963,0.111410934004226,
0.028453244999659));
#18679=CARTESIAN_POINT('Ctrl Pts',(0.106558911742102,0.0797092470962188,
0.0258665863633264));
#18680=CARTESIAN_POINT('Ctrl Pts',(0.11981357554495,0.0409763259700822,
0.0232799277269937));
#18681=CARTESIAN_POINT('Ctrl Pts',(0.133068239347797,0.00224340484394604,
0.0206932690906611));
#18682=CARTESIAN_POINT('Ctrl Pts',(0.125820587496086,-0.0435207505003201,
0.0181066104543285));
#18683=CARTESIAN_POINT('Ctrl Pts',(0.101166903546451,-0.0762076816581678,
0.0155199518179958));
#18684=CARTESIAN_POINT('Ctrl Pts',(0.0765132195968157,-0.108894612816016,
0.0129332931816632));
#18685=CARTESIAN_POINT('Ctrl Pts',(0.0344535035492562,-0.128504319787445,
0.0103466345453306));
#18686=CARTESIAN_POINT('Ctrl Pts',(-0.00636464094143544,-0.126469737202777,
0.00775997590899791));
#18687=CARTESIAN_POINT('Ctrl Pts',(-0.0471827854321269,-0.124435154618108,
0.00517331727266527));
#18688=CARTESIAN_POINT('Ctrl Pts',(-0.0867593583659505,-0.100756282477341,
0.00258665863633259));
#18689=CARTESIAN_POINT('Ctrl Pts',(-0.108089675695031,-0.0656218295092657,
-5.55111512312578E-17));
#18690=CARTESIAN_POINT('Origin',(0.,0.,0.));
#18691=CARTESIAN_POINT('Ctrl Pts',(-0.12639138516214,8.91322620741042E-5,
0.00934196736194174));
#18692=CARTESIAN_POINT('Ctrl Pts',(-0.126154274972366,-0.0296906128949183,
0.011214877787648));
#18693=CARTESIAN_POINT('Ctrl Pts',(-0.115592373032178,-0.0596151635265703,
0.0130877882133543));
#18694=CARTESIAN_POINT('Ctrl Pts',(-0.0963650578556872,-0.0821635787359664,
0.0149606986390606));
#18695=CARTESIAN_POINT('Ctrl Pts',(-0.0698103971670931,-0.113304978845907,
0.0175473572753932));
#18696=CARTESIAN_POINT('Ctrl Pts',(-0.0267272342632827,-0.130377059081323,
0.0201340159117258));
#18697=CARTESIAN_POINT('Ctrl Pts',(0.0139574509341311,-0.125868770046104,
0.0227206745480584));
#18698=CARTESIAN_POINT('Ctrl Pts',(0.0546421361315456,-0.121360481010885,
0.0253073331843911));
#18699=CARTESIAN_POINT('Ctrl Pts',(0.0929283436225635,-0.0952718227050311,
0.0278939918207237));
#18700=CARTESIAN_POINT('Ctrl Pts',(0.112018291148455,-0.0590635258734944,
0.0304806504570564));
#18701=CARTESIAN_POINT('Ctrl Pts',(0.131108238674346,-0.0228552290419586,
0.033067309093389));
#18702=CARTESIAN_POINT('Ctrl Pts',(0.131001926235112,0.0234727063152593,
0.0356539677297216));
#18703=CARTESIAN_POINT('Ctrl Pts',(0.111741771403992,0.0595891814911641,
0.0382406263660542));
#18704=CARTESIAN_POINT('Ctrl Pts',(0.0924816165728724,0.0957056566670696,
0.0408272850023869));
#18705=CARTESIAN_POINT('Ctrl Pts',(0.0540676193498672,0.121610671661662,
0.0434139436387195));
#18706=CARTESIAN_POINT('Ctrl Pts',(0.0133639835211523,0.125930636937597,
0.0460006022750522));
#18707=CARTESIAN_POINT('Ctrl Pts',(-0.0273396523075625,0.130250602213533,
0.0485872609113848));
#18708=CARTESIAN_POINT('Ctrl Pts',(-0.0703329267419868,0.112985517770812,
0.0511739195477175));
#18709=CARTESIAN_POINT('Ctrl Pts',(-0.0967449447385466,0.0817152626609385,
0.0537605781840501));
#18710=CARTESIAN_POINT('Ctrl Pts',(-0.115741878896724,0.0592240248649833,
0.0556210412433473));
#18711=CARTESIAN_POINT('Ctrl Pts',(-0.126160906676814,0.0294875554882879,
0.0574815043026445));
#18712=CARTESIAN_POINT('Ctrl Pts',(-0.126396145829628,-9.95859796292312E-5,
0.0593419673619417));
#18713=CARTESIAN_POINT('Origin',(0.,0.,0.12));
#18714=CARTESIAN_POINT('',(-0.126529791093031,9.025049583615E-5,0.109341967361942));
#18715=CARTESIAN_POINT('',(-0.126349242904067,8.85860673823967E-5,0.0956580326380584));
#18716=CARTESIAN_POINT('',(-0.12645,1.54856587752183E-17,0.12));
#18717=CARTESIAN_POINT('Ctrl Pts',(-0.126349242904067,8.85860673823967E-5,
0.0956580326380584));
#18718=CARTESIAN_POINT('Ctrl Pts',(-0.126441591528965,0.0135570965972842,
0.0948119253946973));
#18719=CARTESIAN_POINT('Ctrl Pts',(-0.124448136217638,0.0269990101701626,
0.0939658181513361));
#18720=CARTESIAN_POINT('Ctrl Pts',(-0.120249444863787,0.0397126388809939,
0.093119710907975));
#18721=CARTESIAN_POINT('Ctrl Pts',(-0.107413505522824,0.0785798365820317,
0.0905330522716423));
#18722=CARTESIAN_POINT('Ctrl Pts',(-0.0739673525896496,0.110640458354997,
0.0879463936353097));
#18723=CARTESIAN_POINT('Ctrl Pts',(-0.0345920580258737,0.121821308595361,
0.085359734998977));
#18724=CARTESIAN_POINT('Ctrl Pts',(0.00478323653790218,0.133002158835724,
0.0827730763626444));
#18725=CARTESIAN_POINT('Ctrl Pts',(0.0500876727322792,0.123303237543486,
0.0801864177263117));
#18726=CARTESIAN_POINT('Ctrl Pts',(0.0814342209129887,0.0969820390626645,
0.077599759089979));
#18727=CARTESIAN_POINT('Ctrl Pts',(0.112780769093698,0.0706608405818426,
0.0750131004536464));
#18728=CARTESIAN_POINT('Ctrl Pts',(0.13016942926074,0.0277173649124373,
0.0724264418173139));
#18729=CARTESIAN_POINT('Ctrl Pts',(0.12596827751407,-0.0129984006283456,
0.0698397831809812));
#18730=CARTESIAN_POINT('Ctrl Pts',(0.121767125767399,-0.0537141661691284,
0.0672531245446486));
#18731=CARTESIAN_POINT('Ctrl Pts',(0.0959761621070158,-0.0922022215812886,
0.0646664659083159));
#18732=CARTESIAN_POINT('Ctrl Pts',(0.059914723710966,-0.111567668284471,
0.0620798072719833));
#18733=CARTESIAN_POINT('Ctrl Pts',(0.0238532853149157,-0.130933114987654,
0.0594931486356506));
#18734=CARTESIAN_POINT('Ctrl Pts',(-0.0224786278168013,-0.131175952981858,
0.056906489999318));
#18735=CARTESIAN_POINT('Ctrl Pts',(-0.0587401909579078,-0.112190380850839,
0.0543198313629853));
#18736=CARTESIAN_POINT('Ctrl Pts',(-0.0950017540990138,-0.0932048087198191,
0.0517331727266527));
#18737=CARTESIAN_POINT('Ctrl Pts',(-0.12119296724951,-0.0549908264635757,
0.0491465140903201));
#18738=CARTESIAN_POINT('Ctrl Pts',(-0.125823286774378,-0.0143210998620416,
0.0465598554539874));
#18739=CARTESIAN_POINT('Ctrl Pts',(-0.126361397696569,-0.0095946821776348,
0.0462592478486778));
#18740=CARTESIAN_POINT('Ctrl Pts',(-0.12660831057823,-0.00483509759607578,
0.0459586402433681));
#18741=CARTESIAN_POINT('Ctrl Pts',(-0.126575671592806,-7.20628672610732E-5,
0.0456580326380584));
#18742=CARTESIAN_POINT('Ctrl Pts',(-0.126396145829628,-9.95859796292312E-5,
0.0593419673619417));
#18743=CARTESIAN_POINT('Ctrl Pts',(-0.12648796685852,-0.0116483513064931,
0.0600681629389771));
#18744=CARTESIAN_POINT('Ctrl Pts',(-0.125028206814926,-0.0231743653405588,
0.0607943585160125));
#18745=CARTESIAN_POINT('Ctrl Pts',(-0.121921363946098,-0.034237873926493,
0.0615205540930479));
#18746=CARTESIAN_POINT('Ctrl Pts',(-0.110855003598394,-0.0736453296270277,
0.0641072127293806));
#18747=CARTESIAN_POINT('Ctrl Pts',(-0.0788915213442898,-0.107184815251071,
0.0666938713657133));
#18748=CARTESIAN_POINT('Ctrl Pts',(-0.0400617348236378,-0.120133683626334,
0.069280530002046));
#18749=CARTESIAN_POINT('Ctrl Pts',(-0.00123194830298627,-0.133082552001597,
0.0718671886383786));
#18750=CARTESIAN_POINT('Ctrl Pts',(0.0444641424842127,-0.125440803128081,
0.0744538472747112));
#18751=CARTESIAN_POINT('Ctrl Pts',(0.0769682295152699,-0.100563001286921,
0.0770405059110438));
#18752=CARTESIAN_POINT('Ctrl Pts',(0.109472316546327,-0.0756851994457607,
0.0796271645473764));
#18753=CARTESIAN_POINT('Ctrl Pts',(0.128784399821243,-0.0335713446369571,
0.0822138231837091));
#18754=CARTESIAN_POINT('Ctrl Pts',(0.126427276285523,0.00729262199647547,
0.0848004818200417));
#18755=CARTESIAN_POINT('Ctrl Pts',(0.124070152749803,0.0481565886299079,
0.0873871404563744));
#18756=CARTESIAN_POINT('Ctrl Pts',(0.100043822403448,0.0877706670879697,
0.0899737990927071));
#18757=CARTESIAN_POINT('Ctrl Pts',(0.0648947831756147,0.108746049780439,
0.0925604577290397));
#18758=CARTESIAN_POINT('Ctrl Pts',(0.0297457439477817,0.129721432472907,
0.0951471163653723));
#18759=CARTESIAN_POINT('Ctrl Pts',(-0.0165260041615291,0.132058119399784,
0.0977337750017049));
#18760=CARTESIAN_POINT('Ctrl Pts',(-0.0536093211433369,0.114730442741844,
0.100320433638038));
#18761=CARTESIAN_POINT('Ctrl Pts',(-0.0906926381251451,0.0974027660839045,
0.10290709227437));
#18762=CARTESIAN_POINT('Ctrl Pts',(-0.11858752397945,0.0604107258411485,
0.105493750910703));
#18763=CARTESIAN_POINT('Ctrl Pts',(-0.12504939731921,0.0199921027543164,
0.108080409547035));
#18764=CARTESIAN_POINT('Ctrl Pts',(-0.126099919499473,0.0134211506765118,
0.108500928818671));
#18765=CARTESIAN_POINT('Ctrl Pts',(-0.126583971845017,0.00675963476331471,
0.108921448090306));
#18766=CARTESIAN_POINT('Ctrl Pts',(-0.126529791093031,9.025049583615E-5,
0.109341967361942));
#18767=CARTESIAN_POINT('Origin',(0.,0.,0.12));
#18768=CARTESIAN_POINT('',(-0.126296536029262,-6.10717992316628E-5,0.159341967361942));
#18769=CARTESIAN_POINT('',(-0.126453631260982,-0.000102348163238207,0.145658032638058));
#18770=CARTESIAN_POINT('',(-0.12645,1.54856587752183E-17,0.12));
#18771=CARTESIAN_POINT('Ctrl Pts',(-0.126453631260982,-0.000102348163238207,
0.145658032638058));
#18772=CARTESIAN_POINT('Ctrl Pts',(-0.126183364177612,0.031552920325249,
0.143665210546026));
#18773=CARTESIAN_POINT('Ctrl Pts',(-0.114073771100105,0.0633928690595716,
0.141672388453994));
#18774=CARTESIAN_POINT('Ctrl Pts',(-0.0925489356314354,0.0864391430514358,
0.139679566361962));
#18775=CARTESIAN_POINT('Ctrl Pts',(-0.0646099631645552,0.116352924063146,
0.13709290772563));
#18776=CARTESIAN_POINT('Ctrl Pts',(-0.0208084524006029,0.131451366650306,
0.134506249089297));
#18777=CARTESIAN_POINT('Ctrl Pts',(0.0196287675426836,0.125106932552633,
0.131919590452964));
#18778=CARTESIAN_POINT('Ctrl Pts',(0.0600659874859703,0.11876249845496,
0.129332931816632));
#18779=CARTESIAN_POINT('Ctrl Pts',(0.097138916608591,0.0909751876724545,
0.126746273180299));
#18780=CARTESIAN_POINT('Ctrl Pts',(0.114574233156503,0.0539423598350403,
0.124159614543967));
#18781=CARTESIAN_POINT('Ctrl Pts',(0.132009549704415,0.0169095319976262,
0.121572955907634));
#18782=CARTESIAN_POINT('Ctrl Pts',(0.129807253677619,-0.0293688128946969,
0.118986297271301));
#18783=CARTESIAN_POINT('Ctrl Pts',(0.108934072954415,-0.0645786240759305,
0.116399638634969));
#18784=CARTESIAN_POINT('Ctrl Pts',(0.0880608922312115,-0.099788435257164,
0.113812979998636));
#18785=CARTESIAN_POINT('Ctrl Pts',(0.0485168268116012,-0.123929712727308,
0.111226321362303));
#18786=CARTESIAN_POINT('Ctrl Pts',(0.00765986125275547,-0.126405537442516,
0.108639662725971));
#18787=CARTESIAN_POINT('Ctrl Pts',(-0.0331971043060904,-0.128881362157723,
0.106053004089638));
#18788=CARTESIAN_POINT('Ctrl Pts',(-0.0753669700041717,-0.109691734117994,
0.103466345453305));
#18789=CARTESIAN_POINT('Ctrl Pts',(-0.100339039978837,-0.0772600332835736,
0.100879686816973));
#18790=CARTESIAN_POINT('Ctrl Pts',(-0.117142637704978,-0.0554368822612891,
0.0991391354240014));
#18791=CARTESIAN_POINT('Ctrl Pts',(-0.126159269908366,-0.0276178718881664,
0.0973985840310299));
#18792=CARTESIAN_POINT('Ctrl Pts',(-0.126349242904067,8.85860673823967E-5,
0.0956580326380584));
#18793=CARTESIAN_POINT('Ctrl Pts',(-0.126529791093031,9.025049583615E-5,
0.109341967361942));
#18794=CARTESIAN_POINT('Ctrl Pts',(-0.126250700293628,-0.0342644551610371,
0.111508106726639));
#18795=CARTESIAN_POINT('Ctrl Pts',(-0.111690189779818,-0.0688279388928191,
0.113674246091336));
#18796=CARTESIAN_POINT('Ctrl Pts',(-0.0867076257192948,-0.092297473337895,
0.115840385456033));
#18797=CARTESIAN_POINT('Ctrl Pts',(-0.0568751199544048,-0.120323220412367,
0.118427044092366));
#18798=CARTESIAN_POINT('Ctrl Pts',(-0.0121812475994092,-0.132529508630403,
0.121013702728699));
#18799=CARTESIAN_POINT('Ctrl Pts',(0.0277554439013372,-0.123558363290506,
0.123600361365031));
#18800=CARTESIAN_POINT('Ctrl Pts',(0.0676921354020838,-0.114587217950609,
0.126187020001364));
#18801=CARTESIAN_POINT('Ctrl Pts',(0.102871646048582,-0.0844386390527785,
0.128773678637697));
#18802=CARTESIAN_POINT('Ctrl Pts',(0.117851793294146,-0.0463464242807743,
0.131360337274029));
#18803=CARTESIAN_POINT('Ctrl Pts',(0.13283194053971,-0.00825420950877041,
0.133946995910362));
#18804=CARTESIAN_POINT('Ctrl Pts',(0.127612724384341,0.0377816411374068,
0.136533654546694));
#18805=CARTESIAN_POINT('Ctrl Pts',(0.104485135941302,0.0715534408109559,
0.139120313183027));
#18806=CARTESIAN_POINT('Ctrl Pts',(0.0813575474982633,0.105325240484505,
0.14170697181936));
#18807=CARTESIAN_POINT('Ctrl Pts',(0.0403215867675544,0.126832989185426,
0.144293630455692));
#18808=CARTESIAN_POINT('Ctrl Pts',(-0.000609841963000384,0.126635909896556,
0.146880289092025));
#18809=CARTESIAN_POINT('Ctrl Pts',(-0.0415412706935549,0.126438830607686,
0.149466947728358));
#18810=CARTESIAN_POINT('Ctrl Pts',(-0.0823681674239554,0.104536923329025,
0.15205360636469));
#18811=CARTESIAN_POINT('Ctrl Pts',(-0.10516942503222,0.0705438627883669,
0.154640265001023));
#18812=CARTESIAN_POINT('Ctrl Pts',(-0.118984510025511,0.0499477610899654,
0.156207499121329));
#18813=CARTESIAN_POINT('Ctrl Pts',(-0.126182304652747,0.0249129445447297,
0.157774733241635));
#18814=CARTESIAN_POINT('Ctrl Pts',(-0.126296536029262,-6.10717992316628E-5,
0.159341967361942));
#18815=CARTESIAN_POINT('Origin',(0.,0.,0.12));
#18816=CARTESIAN_POINT('',(-0.126625441102054,2.7778768752873E-5,0.209341967361942));
#18817=CARTESIAN_POINT('',(-0.126471935391749,0.000101176582396995,0.195658032638058));
#18818=CARTESIAN_POINT('',(-0.12645,1.54856587752183E-17,0.12));
#18819=CARTESIAN_POINT('',(0.0958116152722397,0.0825211298936481,0.24));
#18820=CARTESIAN_POINT('Ctrl Pts',(-0.126625441102054,2.7778768752873E-5,
0.209341967361942));
#18821=CARTESIAN_POINT('Ctrl Pts',(-0.126482885932031,-0.0388928622545336,
0.21180133566563));
#18822=CARTESIAN_POINT('Ctrl Pts',(-0.107125339127294,-0.077921419747323,
0.214260703969318));
#18823=CARTESIAN_POINT('Ctrl Pts',(-0.0759952538809665,-0.101287130411732,
0.216720072273006));
#18824=CARTESIAN_POINT('Ctrl Pts',(-0.0432539585932993,-0.12586218783339,
0.219306730909339));
#18825=CARTESIAN_POINT('Ctrl Pts',(0.0025100419330305,-0.133111106253138,
0.221893389545672));
#18826=CARTESIAN_POINT('Ctrl Pts',(0.0412155518054008,-0.119764891216682,
0.224480048182004));
#18827=CARTESIAN_POINT('Ctrl Pts',(0.0799210616777711,-0.106418676180227,
0.227066706818337));
#18828=CARTESIAN_POINT('Ctrl Pts',(0.111568080896182,-0.072477327687567,
0.229653365454669));
#18829=CARTESIAN_POINT('Ctrl Pts',(0.122246574267713,-0.0330282462555153,
0.232240024091002));
#18830=CARTESIAN_POINT('Ctrl Pts',(0.132925067639245,0.00642083517653631,
0.234826682727335));
#18831=CARTESIAN_POINT('Ctrl Pts',(0.122635035163896,0.0513776495479799,
0.237413341363667));
#18832=CARTESIAN_POINT('Ctrl Pts',(0.0958116152722397,0.0825211298936481,
0.24));
#18833=CARTESIAN_POINT('',(-0.0959791030802601,0.0826138105732953,0.24));
#18834=CARTESIAN_POINT('Origin',(0.,0.,0.24));
#18835=CARTESIAN_POINT('Ctrl Pts',(-0.0959791030802601,0.0826138105732953,
0.24));
#18836=CARTESIAN_POINT('Ctrl Pts',(-0.0710417758635208,0.111296717646776,
0.237599759089979));
#18837=CARTESIAN_POINT('Ctrl Pts',(-0.0322351762885183,0.128218895525122,
0.235199518179958));
#18838=CARTESIAN_POINT('Ctrl Pts',(0.00571352152256588,0.126497857083363,
0.232799277269937));
#18839=CARTESIAN_POINT('Ctrl Pts',(0.0466095526337785,0.124643152028446,
0.230212618633605));
#18840=CARTESIAN_POINT('Ctrl Pts',(0.0865092470399708,0.101136876245298,
0.227625959997272));
#18841=CARTESIAN_POINT('Ctrl Pts',(0.107920636628548,0.0662586835305903,
0.225039301360939));
#18842=CARTESIAN_POINT('Ctrl Pts',(0.129332026217125,0.0313804908158828,
0.222452642724607));
#18843=CARTESIAN_POINT('Ctrl Pts',(0.132255110988087,-0.014869618830384,
0.219865984088274));
#18844=CARTESIAN_POINT('Ctrl Pts',(0.115395215428634,-0.0521699181865619,
0.217279325451942));
#18845=CARTESIAN_POINT('Ctrl Pts',(0.0985353198691812,-0.0894702175427398,
0.214692666815609));
#18846=CARTESIAN_POINT('Ctrl Pts',(0.0618924439793129,-0.117820706608829,
0.212106008179276));
#18847=CARTESIAN_POINT('Ctrl Pts',(0.0215571925812854,-0.12478734248304,
0.209519349542944));
#18848=CARTESIAN_POINT('Ctrl Pts',(-0.0187780588167422,-0.13175397835725,
0.206932690906611));
#18849=CARTESIAN_POINT('Ctrl Pts',(-0.0628056857229291,-0.117336761039583,
0.204346032270278));
#18850=CARTESIAN_POINT('Ctrl Pts',(-0.0912027768750998,-0.0878586653637446,
0.201759373633946));
#18851=CARTESIAN_POINT('Ctrl Pts',(-0.113530209130371,-0.0646812849521466,
0.199725593301983));
#18852=CARTESIAN_POINT('Ctrl Pts',(-0.126194825294183,-0.0321932513395888,
0.197691812970021));
#18853=CARTESIAN_POINT('Ctrl Pts',(-0.126471935391749,0.000101176582396995,
0.195658032638058));
#18854=CARTESIAN_POINT('Origin',(0.,0.,0.350421172358873));
#18855=CARTESIAN_POINT('',(-0.154453350152392,-8.79343647196378E-5,0.0295788276411275));
#18856=CARTESIAN_POINT('',(-0.15422847552802,0.000108763211052777,0.025421172358873));
#18857=CARTESIAN_POINT('',(-0.1543,-1.01731279388251E-15,0.350421172358873));
#18858=CARTESIAN_POINT('',(0.15408394018464,-0.00816268198427004,0.));
#18859=CARTESIAN_POINT('Ctrl Pts',(-0.15422847552802,0.000108763211052763,
0.025421172358873));
#18860=CARTESIAN_POINT('Ctrl Pts',(-0.154338737393477,0.0139570514561378,
0.0247074241482466));
#18861=CARTESIAN_POINT('Ctrl Pts',(-0.146387882101843,0.0778735560251454,
0.0214070173012875));
#18862=CARTESIAN_POINT('Ctrl Pts',(-0.0581466660421577,0.171532975008042,
0.0155199518179959));
#18863=CARTESIAN_POINT('Ctrl Pts',(0.109502662757235,0.144085240745689,
0.00775997590899784));
#18864=CARTESIAN_POINT('Ctrl Pts',(0.156737212705124,0.0419221657566679,
0.00258665863633264));
#18865=CARTESIAN_POINT('Ctrl Pts',(0.15408394018464,-0.00816268198427004,
0.));
#18866=CARTESIAN_POINT('',(0.129620323775263,-0.0841289546921688,3.62607491890453E-17));
#18867=CARTESIAN_POINT('Origin',(0.,0.,0.));
#18868=CARTESIAN_POINT('Ctrl Pts',(-0.154453350152392,-8.7934364719636E-5,
0.0295788276411275));
#18869=CARTESIAN_POINT('Ctrl Pts',(-0.154150470777978,0.0441115087317509,
0.0272927766101045));
#18870=CARTESIAN_POINT('Ctrl Pts',(-0.111454882743928,0.138841433785012,
0.0224200669427489));
#18871=CARTESIAN_POINT('Ctrl Pts',(0.0476444145610997,0.174632482457551,
0.0149606986390605));
#18872=CARTESIAN_POINT('Ctrl Pts',(0.168251138196633,0.0613688951001999,
0.0073871404563744));
#18873=CARTESIAN_POINT('Ctrl Pts',(0.154676764047789,-0.0451013867871701,
0.00240024091002087));
#18874=CARTESIAN_POINT('Ctrl Pts',(0.129620323775263,-0.0841289546921688,
1.57209315010398E-17));
#18875=CARTESIAN_POINT('Origin',(0.,0.,0.350421172358873));
#18876=CARTESIAN_POINT('',(-0.154177051641736,0.000108096719625833,0.0795788276411275));
#18877=CARTESIAN_POINT('',(-0.154234284709463,-0.000121519309271207,0.075421172358873));
#18878=CARTESIAN_POINT('',(-0.1543,-1.01731279388251E-15,0.350421172358873));
#18879=CARTESIAN_POINT('Ctrl Pts',(-0.154234284709463,-0.000121519309271208,
0.0754211723588731));
#18880=CARTESIAN_POINT('Ctrl Pts',(-0.153947235272697,0.0359820467524117,
0.0735607092995758));
#18881=CARTESIAN_POINT('Ctrl Pts',(-0.123557126730793,0.122717061869437,
0.0691135876039459));
#18882=CARTESIAN_POINT('Ctrl Pts',(0.0191012565771036,0.180005302104073,
0.0620798072719832));
#18883=CARTESIAN_POINT('Ctrl Pts',(0.159724738700703,0.0851738948996701,
0.0543198313629854));
#18884=CARTESIAN_POINT('Ctrl Pts',(0.160113920417758,-0.0844204212478698,
0.0465598554539874));
#18885=CARTESIAN_POINT('Ctrl Pts',(0.0199582426985643,-0.179924098035372,
0.0387998795449896));
#18886=CARTESIAN_POINT('Ctrl Pts',(-0.123251388539896,-0.123176028715441,
0.0317536518466181));
#18887=CARTESIAN_POINT('Ctrl Pts',(-0.153939142967466,-0.0362298265692857,
0.0272940827845792));
#18888=CARTESIAN_POINT('Ctrl Pts',(-0.15422847552802,0.000108763211052763,
0.025421172358873));
#18889=CARTESIAN_POINT('Ctrl Pts',(-0.154177051641736,0.000108096719625859,
0.0795788276411275));
#18890=CARTESIAN_POINT('Ctrl Pts',(-0.154289739603949,0.0165429814548096,
0.0787327203977663));
#18891=CARTESIAN_POINT('Ctrl Pts',(-0.144420757340354,0.0830897487115299,
0.0752999545180725));
#18892=CARTESIAN_POINT('Ctrl Pts',(-0.0494457976037486,0.174130301808973,
0.0692805300020459));
#18893=CARTESIAN_POINT('Ctrl Pts',(0.11640175885633,0.13862511662766,0.061520554093048));
#18894=CARTESIAN_POINT('Ctrl Pts',(0.18005704388064,-0.0185795878987759,
0.0537605781840501));
#18895=CARTESIAN_POINT('Ctrl Pts',(0.0856431484406112,-0.159474177462153,
0.0460006022750521));
#18896=CARTESIAN_POINT('Ctrl Pts',(-0.0839657292871194,-0.160363143120653,
0.0382406263660544));
#18897=CARTESIAN_POINT('Ctrl Pts',(-0.151599316432495,-0.0616831513139142,
0.0327667014880793));
#18898=CARTESIAN_POINT('Ctrl Pts',(-0.154493177716258,-0.00590000442131094,
0.0298794352464371));
#18899=CARTESIAN_POINT('Ctrl Pts',(-0.154453350152392,-8.7934364719636E-5,
0.0295788276411275));
#18900=CARTESIAN_POINT('Origin',(0.,0.,0.350421172358873));
#18901=CARTESIAN_POINT('',(-0.154304431028624,-0.000124889850439479,0.129578827641127));
#18902=CARTESIAN_POINT('',(-0.154397364694779,0.000110127730384366,0.125421172358873));
#18903=CARTESIAN_POINT('',(-0.1543,-1.01731279388251E-15,0.350421172358873));
#18904=CARTESIAN_POINT('Ctrl Pts',(-0.154397364694779,0.000110127730384357,
0.125421172358873));
#18905=CARTESIAN_POINT('Ctrl Pts',(-0.154463478494948,0.00824841157753406,
0.125000653087238));
#18906=CARTESIAN_POINT('Ctrl Pts',(-0.150239588102603,0.0663774823757793,
0.121993475179269));
#18907=CARTESIAN_POINT('Ctrl Pts',(-0.0766286530280003,0.163994611436961,
0.116399638634969));
#18908=CARTESIAN_POINT('Ctrl Pts',(0.0927599764682439,0.155440618724813,
0.108639662725971));
#18909=CARTESIAN_POINT('Ctrl Pts',(0.180714016146597,0.0104239566588842,
0.100879686816973));
#18910=CARTESIAN_POINT('Ctrl Pts',(0.11001758793024,-0.143743725357685,
0.093119710907975));
#18911=CARTESIAN_POINT('Ctrl Pts',(-0.0572637123892103,-0.171718146500831,
0.0853597349989769));
#18912=CARTESIAN_POINT('Ctrl Pts',(-0.146220320052713,-0.0783754111826042,
0.0794602221492764));
#18913=CARTESIAN_POINT('Ctrl Pts',(-0.154346328875204,-0.0142138442593302,
0.0761473679359084));
#18914=CARTESIAN_POINT('Ctrl Pts',(-0.154234284709463,-0.000121519309271208,
0.0754211723588731));
#18915=CARTESIAN_POINT('Ctrl Pts',(-0.154304431028624,-0.000124889850439474,
0.129578827641127));
#18916=CARTESIAN_POINT('Ctrl Pts',(-0.153974638929265,0.0385022981904757,
0.127586005549095));
#18917=CARTESIAN_POINT('Ctrl Pts',(-0.120018027207353,0.127784966030512,
0.123006524820731));
#18918=CARTESIAN_POINT('Ctrl Pts',(0.0280571680938306,0.178826694862324,
0.115840385456033));
#18919=CARTESIAN_POINT('Ctrl Pts',(0.163771354656592,0.0771047007047774,
0.108080409547035));
#18920=CARTESIAN_POINT('Ctrl Pts',(0.155709331479018,-0.0923080778690166,
0.100320433638038));
#18921=CARTESIAN_POINT('Ctrl Pts',(0.0109489686262093,-0.180682908560435,
0.0925604577290397));
#18922=CARTESIAN_POINT('Ctrl Pts',(-0.126591758993125,-0.118094248159534,
0.0856465890634029));
#18923=CARTESIAN_POINT('Ctrl Pts',(-0.153945238013925,-0.0337005743957639,
0.0813193790340989));
#18924=CARTESIAN_POINT('Ctrl Pts',(-0.154177051641736,0.000108096719625859,
0.0795788276411275));
#18925=CARTESIAN_POINT('Origin',(0.,0.,0.350421172358873));
#18926=CARTESIAN_POINT('',(-0.154326766555531,0.000123460234585843,0.179578827641127));
#18927=CARTESIAN_POINT('',(-0.154112736333057,-7.45225671948511E-5,0.175421172358873));
#18928=CARTESIAN_POINT('',(-0.1543,-1.01731279388251E-15,0.350421172358873));
#18929=CARTESIAN_POINT('Ctrl Pts',(-0.154112736333057,-7.45225671948471E-5,
0.175421172358873));
#18930=CARTESIAN_POINT('Ctrl Pts',(-0.153973346049181,0.0303998999070902,
0.173853938238567));
#18931=CARTESIAN_POINT('Ctrl Pts',(-0.130694151755309,0.111367805862998,
0.169700045481928));
#18932=CARTESIAN_POINT('Ctrl Pts',(-0.000871711368246156,0.181012066871201,
0.162959494088956));
#18933=CARTESIAN_POINT('Ctrl Pts',(0.149350085565286,0.102277888352765,
0.155199518179958));
#18934=CARTESIAN_POINT('Ctrl Pts',(0.168456255263351,-0.0662471829332422,
0.14743954227096));
#18935=CARTESIAN_POINT('Ctrl Pts',(0.0396733728729688,-0.17661315503135,
0.139679566361963));
#18936=CARTESIAN_POINT('Ctrl Pts',(-0.115072782317819,-0.134350623919955,
0.1323401097246));
#18937=CARTESIAN_POINT('Ctrl Pts',(-0.154056805498669,-0.041811035439686,
0.12758731172357));
#18938=CARTESIAN_POINT('Ctrl Pts',(-0.154397364694779,0.000110127730384357,
0.125421172358873));
#18939=CARTESIAN_POINT('Ctrl Pts',(-0.154326766555531,0.000123460234585825,
0.179578827641127));
#18940=CARTESIAN_POINT('Ctrl Pts',(-0.154418689716183,0.0108361910665024,
0.179025949336757));
#18941=CARTESIAN_POINT('Ctrl Pts',(-0.148597337680631,0.071569631208062,
0.175886412396054));
#18942=CARTESIAN_POINT('Ctrl Pts',(-0.0683530255288039,0.167611467503216,
0.170160216819019));
#18943=CARTESIAN_POINT('Ctrl Pts',(0.100397202365132,0.150621028353064,
0.162400240910021));
#18944=CARTESIAN_POINT('Ctrl Pts',(0.18100910679194,0.00139719974911195,
0.154640265001023));
#18945=CARTESIAN_POINT('Ctrl Pts',(0.102711092909207,-0.149052183789333,
0.146880289092025));
#18946=CARTESIAN_POINT('Ctrl Pts',(-0.0657574679958034,-0.168648048308422,
0.139120313183027));
#18947=CARTESIAN_POINT('Ctrl Pts',(-0.148058381688037,-0.0731761882111772,
0.133353159366061));
#18948=CARTESIAN_POINT('Ctrl Pts',(-0.154402705029802,-0.0116353181791797,
0.130172664185428));
#18949=CARTESIAN_POINT('Ctrl Pts',(-0.154304431028624,-0.000124889850439474,
0.129578827641127));
#18950=CARTESIAN_POINT('Origin',(0.,0.,0.350421172358873));
#18951=CARTESIAN_POINT('',(-0.154128406284035,-0.000157308197905263,0.229578827641128));
#18952=CARTESIAN_POINT('',(-0.154514081154978,3.38969080117728E-5,0.225421172358873));
#18953=CARTESIAN_POINT('',(-0.1543,-1.01731279388251E-15,0.350421172358873));
#18954=CARTESIAN_POINT('',(-0.0398513841857245,-0.149064942821851,0.24));
#18955=CARTESIAN_POINT('Ctrl Pts',(-0.0398513841857245,-0.149064942821851,
0.24));
#18956=CARTESIAN_POINT('Ctrl Pts',(-0.0883048112969314,-0.136111285829332,
0.237413341363667));
#18957=CARTESIAN_POINT('Ctrl Pts',(-0.143745772087175,-0.0847488633265083,
0.233939617244043));
#18958=CARTESIAN_POINT('Ctrl Pts',(-0.154234229255939,-0.017399338864059,
0.230465893124419));
#18959=CARTESIAN_POINT('Ctrl Pts',(-0.154128406284035,-0.00015730819790527,
0.229578827641128));
#18960=CARTESIAN_POINT('',(0.0399565498027962,-0.149273502906638,0.24));
#18961=CARTESIAN_POINT('Origin',(0.,0.,0.24));
#18962=CARTESIAN_POINT('Ctrl Pts',(0.0399565498027963,-0.149273502906638,
0.24));
#18963=CARTESIAN_POINT('Ctrl Pts',(-0.00490373130458673,-0.161043406468747,
0.237599759089979));
#18964=CARTESIAN_POINT('Ctrl Pts',(-0.107666111297752,-0.141562671532916,
0.23274014987627));
#18965=CARTESIAN_POINT('Ctrl Pts',(-0.154340128899266,-0.0474588267763927,
0.227880540662561));
#18966=CARTESIAN_POINT('Ctrl Pts',(-0.154514081154978,3.3896908011755E-5,
0.225421172358873));
#18967=CARTESIAN_POINT('Origin',(0.,0.,0.350421172358873));
#18968=CARTESIAN_POINT('Ctrl Pts',(-0.154514081154978,3.3896908011755E-5,
0.225421172358873));
#18969=CARTESIAN_POINT('Ctrl Pts',(-0.154523084458981,0.00249199339844659,
0.225293882026228));
#18970=CARTESIAN_POINT('Ctrl Pts',(-0.153375868586475,0.0548933889046004,
0.222579933057251));
#18971=CARTESIAN_POINT('Ctrl Pts',(-0.0942515706791253,0.154556313135293,
0.217279325451942));
#18972=CARTESIAN_POINT('Ctrl Pts',(0.0750450248431312,0.164716481511431,
0.209519349542944));
#18973=CARTESIAN_POINT('Ctrl Pts',(0.178461260043253,0.0303012077178856,
0.201759373633945));
#18974=CARTESIAN_POINT('Ctrl Pts',(0.125203781387627,-0.130731709675357,
0.193999397724948));
#18975=CARTESIAN_POINT('Ctrl Pts',(-0.0379704533096903,-0.17698585337688,
0.18623942181595));
#18976=CARTESIAN_POINT('Ctrl Pts',(-0.141587477595567,-0.0899051669249145,
0.180046680027258));
#18977=CARTESIAN_POINT('Ctrl Pts',(-0.154203404262525,-0.019896942829432,
0.176440596874899));
#18978=CARTESIAN_POINT('Ctrl Pts',(-0.154112736333057,-7.45225671948471E-5,
0.175421172358873));
#18979=CARTESIAN_POINT('Ctrl Pts',(-0.154128406284035,-0.00015730819790527,
0.229578827641128));
#18980=CARTESIAN_POINT('Ctrl Pts',(-0.153925652370292,0.0328779499839183,
0.227879234488086));
#18981=CARTESIAN_POINT('Ctrl Pts',(-0.127638532780061,0.116591914860373,
0.223592982698713));
#18982=CARTESIAN_POINT('Ctrl Pts',(0.00818767200092134,0.180778621679153,
0.216720072273006));
#18983=CARTESIAN_POINT('Ctrl Pts',(0.154249898498561,0.0947283641859207,
0.208960096364008));
#18984=CARTESIAN_POINT('Ctrl Pts',(0.164950538597243,-0.0745810526211722,
0.201200120455011));
#18985=CARTESIAN_POINT('Ctrl Pts',(0.0308106631569891,-0.178364693496558,
0.193440144546012));
#18986=CARTESIAN_POINT('Ctrl Pts',(-0.118879635670858,-0.129347344159377,
0.186233046941385));
#18987=CARTESIAN_POINT('Ctrl Pts',(-0.153988624301243,-0.0392836590090855,
0.18161260797309));
#18988=CARTESIAN_POINT('Ctrl Pts',(-0.154326766555531,0.000123460234585825,
0.179578827641127));
#18989=CARTESIAN_POINT('Ctrl Pts',(0.0958116152722397,0.0825211298936481,
0.24));
#18990=CARTESIAN_POINT('Ctrl Pts',(0.122635035163896,0.0513776495479799,
0.237413341363667));
#18991=CARTESIAN_POINT('Ctrl Pts',(0.143215100114593,-0.0385359791949074,
0.232240024091002));
#18992=CARTESIAN_POINT('Ctrl Pts',(0.0482740424593604,-0.140360024672886,
0.224480048182004));
#18993=CARTESIAN_POINT('Ctrl Pts',(-0.0890179591196291,-0.118613269413641,
0.216720072273006));
#18994=CARTESIAN_POINT('Ctrl Pts',(-0.148173729266643,0.00709031985706173,
0.208960096364008));
#18995=CARTESIAN_POINT('Ctrl Pts',(-0.0772398646297824,0.126660050524678,
0.20120012045501));
#18996=CARTESIAN_POINT('Ctrl Pts',(0.0614999571705377,0.134986384232796,
0.193440144546013));
#18997=CARTESIAN_POINT('Ctrl Pts',(0.146250332679645,0.0248320655601208,
0.185680168637014));
#18998=CARTESIAN_POINT('Ctrl Pts',(0.102605431992647,-0.107135610424167,
0.177920192728017));
#18999=CARTESIAN_POINT('Ctrl Pts',(-0.0311170694815965,-0.145041225920327,
0.170160216819019));
#19000=CARTESIAN_POINT('Ctrl Pts',(-0.137521919612742,-0.0556176253575994,
0.162400240910021));
#19001=CARTESIAN_POINT('Ctrl Pts',(-0.123195064154356,0.0826350160503635,
0.154640265001023));
#19002=CARTESIAN_POINT('Ctrl Pts',(-0.000714373963154436,0.148340737886347,
0.146880289092025));
#19003=CARTESIAN_POINT('Ctrl Pts',(0.122393508228972,0.0838174917835845,
0.139120313183027));
#19004=CARTESIAN_POINT('Ctrl Pts',(0.138051156695079,-0.0542900601549481,
0.131360337274029));
#19005=CARTESIAN_POINT('Ctrl Pts',(0.032512624755586,-0.14473579684844,
0.123600361365031));
#19006=CARTESIAN_POINT('Ctrl Pts',(-0.101568992309399,-0.108116932194331,
0.115840385456033));
#19007=CARTESIAN_POINT('Ctrl Pts',(-0.146482409833755,0.0234186855983926,
0.108080409547036));
#19008=CARTESIAN_POINT('Ctrl Pts',(-0.0627977522708403,0.13439480632666,
0.100320433638038));
#19009=CARTESIAN_POINT('Ctrl Pts',(0.076017492057093,0.127384745546031,
0.0925604577290397));
#19010=CARTESIAN_POINT('Ctrl Pts',(0.148096483096158,0.00854251017184644,
0.0848004818200417));
#19011=CARTESIAN_POINT('Ctrl Pts',(0.0901602332714121,-0.117799054254564,
0.0770405059110438));
#19012=CARTESIAN_POINT('Ctrl Pts',(-0.0469280390901857,-0.140724300875114,
0.069280530002046));
#19013=CARTESIAN_POINT('Ctrl Pts',(-0.142818485852497,-0.0401058440029853,
0.0615205540930479));
#19014=CARTESIAN_POINT('Ctrl Pts',(-0.113326201176411,0.0957204333280909,
0.0537605781840501));
#19015=CARTESIAN_POINT('Ctrl Pts',(0.0156536221268617,0.147515686656254,
0.0460006022750521));
#19016=CARTESIAN_POINT('Ctrl Pts',(0.130895613795878,0.0698006416724775,
0.0382406263660543));
#19017=CARTESIAN_POINT('Ctrl Pts',(0.13121455111358,-0.0691831643991777,
0.0304806504570563));
#19018=CARTESIAN_POINT('Ctrl Pts',(0.0163559286405278,-0.147449139316739,
0.0227206745480584));
#19019=CARTESIAN_POINT('Ctrl Pts',(-0.112893560070904,-0.0962328986104914,
0.0149606986390606));
#19020=CARTESIAN_POINT('Ctrl Pts',(-0.142972035491037,0.0393992613429074,
0.00720072273006258));
#19021=CARTESIAN_POINT('Ctrl Pts',(-0.0476516261894416,0.140572551456688,
-0.000559253178935252));
#19022=CARTESIAN_POINT('Ctrl Pts',(0.0897382482543901,0.118078928660352,
-0.00831922908793326));
#19023=CARTESIAN_POINT('Ctrl Pts',(0.128447313976429,0.0343555272840613,
-0.0134925463605985));
#19024=CARTESIAN_POINT('Ctrl Pts',(0.126272937371016,-0.00668937872268922,
-0.0160792049969311));
#19025=CARTESIAN_POINT('Ctrl Pts',(0.102845629995666,0.0885794229410663,
0.245359734998977));
#19026=CARTESIAN_POINT('Ctrl Pts',(0.13163829265517,0.0551495423644061,
0.242773076362644));
#19027=CARTESIAN_POINT('Ctrl Pts',(0.153729244145676,-0.0413651001137901,
0.237599759089979));
#19028=CARTESIAN_POINT('Ctrl Pts',(0.0518180837997932,-0.150664563191773,
0.229839783180981));
#19029=CARTESIAN_POINT('Ctrl Pts',(-0.0955532172229155,-0.127321268762976,
0.222079807271983));
#19030=CARTESIAN_POINT('Ctrl Pts',(-0.159051911315084,0.00761085605850937,
0.214319831362985));
#19031=CARTESIAN_POINT('Ctrl Pts',(-0.0829104333128967,0.135958804728216,
0.206559855453988));
#19032=CARTESIAN_POINT('Ctrl Pts',(0.0660149797280689,0.144896416659008,
0.19879987954499));
#19033=CARTESIAN_POINT('Ctrl Pts',(0.156987308467515,0.0266551129460425,
0.191039903635992));
#19034=CARTESIAN_POINT('Ctrl Pts',(0.110138215124307,-0.11500097684123,
0.183279927726994));
#19035=CARTESIAN_POINT('Ctrl Pts',(-0.0334015307576278,-0.155689435072511,
0.175519951817996));
#19036=CARTESIAN_POINT('Ctrl Pts',(-0.147618098500879,-0.0597007962188336,
0.167759975908998));
#19037=CARTESIAN_POINT('Ctrl Pts',(-0.13223943620312,0.0887016700559064,
0.16));
#19038=CARTESIAN_POINT('Ctrl Pts',(-0.000766819764851659,0.159231180881298,
0.152240024091002));
#19039=CARTESIAN_POINT('Ctrl Pts',(0.131379034007743,0.0899709573066447,
0.144480048182004));
#19040=CARTESIAN_POINT('Ctrl Pts',(0.14818618955117,-0.0582757677477129,
0.136720072273006));
#19041=CARTESIAN_POINT('Ctrl Pts',(0.0348995407947136,-0.15536158290941,
0.128960096364009));
#19042=CARTESIAN_POINT('Ctrl Pts',(-0.109025685167754,-0.116054342400242,
0.12120012045501));
#19043=CARTESIAN_POINT('Ctrl Pts',(-0.157236423577976,0.0251379696208395,
0.113440144546013));
#19044=CARTESIAN_POINT('Ctrl Pts',(-0.0674080525232269,0.144261408030094,
0.105680168637014));
#19045=CARTESIAN_POINT('Ctrl Pts',(0.0815983201941432,0.136736703272292,
0.0979201927280168));
#19046=CARTESIAN_POINT('Ctrl Pts',(0.158968994112971,0.00916965900085902,
0.0901602168190187));
#19047=CARTESIAN_POINT('Ctrl Pts',(0.0967793514910216,-0.126447277955604,
0.0824002409100209));
#19048=CARTESIAN_POINT('Ctrl Pts',(-0.0503732635231939,-0.151055582750353,
0.0746402650010229));
#19049=CARTESIAN_POINT('Ctrl Pts',(-0.15330351242688,-0.0430502166284845,
0.066880289092025));
#19050=CARTESIAN_POINT('Ctrl Pts',(-0.121646050135849,0.102747753924341,
0.0591203131830272));
#19051=CARTESIAN_POINT('Ctrl Pts',(0.0168028336102756,0.158345558472194,
0.0513603372740292));
#19052=CARTESIAN_POINT('Ctrl Pts',(0.140505322097486,0.074925059414875,
0.0436003613650313));
#19053=CARTESIAN_POINT('Ctrl Pts',(0.140847674214973,-0.0742622500154084,
0.0358403854560334));
#19054=CARTESIAN_POINT('Ctrl Pts',(0.0175566999932067,-0.158274125556283,
0.0280804095470355));
#19055=CARTESIAN_POINT('Ctrl Pts',(-0.121181646661057,-0.103297841872129,
0.0203204336380376));
#19056=CARTESIAN_POINT('Ctrl Pts',(-0.153468334920127,0.0422917601656304,
0.0125604577290396));
#19057=CARTESIAN_POINT('Ctrl Pts',(-0.0511499728070136,0.150892692640473,
0.00480048182004178));
#19058=CARTESIAN_POINT('Ctrl Pts',(0.0963263864220051,0.126747699355464,
-0.00295949408895622));
#19059=CARTESIAN_POINT('Ctrl Pts',(0.137877280219327,0.0368777401082635,
-0.00813281136162143));
#19060=CARTESIAN_POINT('Ctrl Pts',(0.135543271642224,-0.00718047980988283,
-0.0107194699979541));
#19061=CARTESIAN_POINT('Ctrl Pts',(0.109879644719093,0.0946377159884845,
0.250719469997954));
#19062=CARTESIAN_POINT('Ctrl Pts',(0.140641550146443,0.0589214351808321,
0.248132811361621));
#19063=CARTESIAN_POINT('Ctrl Pts',(0.164243388176759,-0.0441942210326729,
0.242959494088956));
#19064=CARTESIAN_POINT('Ctrl Pts',(0.055362125140226,-0.160969101710661,
0.235199518179958));
#19065=CARTESIAN_POINT('Ctrl Pts',(-0.102088475326202,-0.13602926811231,
0.227439542270961));
#19066=CARTESIAN_POINT('Ctrl Pts',(-0.169930093363525,0.00813139225995705,
0.219679566361962));
#19067=CARTESIAN_POINT('Ctrl Pts',(-0.0885810019960112,0.145257558931755,
0.211919590452965));
#19068=CARTESIAN_POINT('Ctrl Pts',(0.0705300022856002,0.154806449085219,
0.204159614543967));
#19069=CARTESIAN_POINT('Ctrl Pts',(0.167724284255384,0.0284781603319641,
0.196399638634969));
#19070=CARTESIAN_POINT('Ctrl Pts',(0.117670998255967,-0.122866343258294,
0.188639662725971));
#19071=CARTESIAN_POINT('Ctrl Pts',(-0.0356859920336591,-0.166337644224695,
0.180879686816973));
#19072=CARTESIAN_POINT('Ctrl Pts',(-0.157714277389017,-0.0637839670800676,
0.173119710907975));
#19073=CARTESIAN_POINT('Ctrl Pts',(-0.141283808251885,0.0947683240614489,
0.165359734998977));
#19074=CARTESIAN_POINT('Ctrl Pts',(-0.000819265566548849,0.17012162387625,
0.157599759089979));
#19075=CARTESIAN_POINT('Ctrl Pts',(0.140364559786514,0.0961244228297045,
0.149839783180981));
#19076=CARTESIAN_POINT('Ctrl Pts',(0.158321222407261,-0.0622614753404775,
0.142079807271983));
#19077=CARTESIAN_POINT('Ctrl Pts',(0.0372864568338413,-0.16598736897038,
0.134319831362986));
#19078=CARTESIAN_POINT('Ctrl Pts',(-0.116482378026109,-0.123991752606152,
0.126559855453987));
#19079=CARTESIAN_POINT('Ctrl Pts',(-0.167990437322196,0.0268572536432864,
0.11879987954499));
#19080=CARTESIAN_POINT('Ctrl Pts',(-0.0720183527756138,0.154128009733527,
0.111039903635992));
#19081=CARTESIAN_POINT('Ctrl Pts',(0.0871791483311938,0.146088660998552,
0.103279927726994));
#19082=CARTESIAN_POINT('Ctrl Pts',(0.169841505129784,0.00979680782987164,
0.0955199518179957));
#19083=CARTESIAN_POINT('Ctrl Pts',(0.103398469710631,-0.135095501656644,
0.0877599759089979));
#19084=CARTESIAN_POINT('Ctrl Pts',(-0.0538184879562023,-0.161386864625592,
0.08));
#19085=CARTESIAN_POINT('Ctrl Pts',(-0.163788539001263,-0.0459945892539838,
0.0722400240910021));
#19086=CARTESIAN_POINT('Ctrl Pts',(-0.129965899095288,0.10977507452059,
0.0644800481820042));
#19087=CARTESIAN_POINT('Ctrl Pts',(0.0179520450936897,0.169175430288133,
0.0567200722730062));
#19088=CARTESIAN_POINT('Ctrl Pts',(0.150115030399095,0.0800494771572726,
0.0489600963640084));
#19089=CARTESIAN_POINT('Ctrl Pts',(0.150480797316365,-0.0793413356316391,
0.0412001204550104));
#19090=CARTESIAN_POINT('Ctrl Pts',(0.0187574713458855,-0.169099111795828,
0.0334401445460125));
#19091=CARTESIAN_POINT('Ctrl Pts',(-0.129469733251211,-0.110362785133767,
0.0256801686370146));
#19092=CARTESIAN_POINT('Ctrl Pts',(-0.163964634349217,0.0451842589883535,
0.0179201927280167));
#19093=CARTESIAN_POINT('Ctrl Pts',(-0.0546483194245858,0.161212833824257,
0.0101602168190188));
#19094=CARTESIAN_POINT('Ctrl Pts',(0.10291452458962,0.135416470050577,0.00240024091002082));
#19095=CARTESIAN_POINT('Ctrl Pts',(0.147307246462226,0.0393999529324658,
-0.00277307636264439));
#19096=CARTESIAN_POINT('Ctrl Pts',(0.144813605913432,-0.00767158089707644,
-0.00535973499897704));
#19097=CARTESIAN_POINT('Ctrl Pts',(0.116913659442519,0.100696009035903,
0.256079204996931));
#19098=CARTESIAN_POINT('Ctrl Pts',(0.149644807637716,0.0626933279972582,
0.253492546360598));
#19099=CARTESIAN_POINT('Ctrl Pts',(0.174757532207842,-0.0470233419515556,
0.248319229087933));
#19100=CARTESIAN_POINT('Ctrl Pts',(0.0589061664806588,-0.171273640229548,
0.240559253178935));
#19101=CARTESIAN_POINT('Ctrl Pts',(-0.108623733429488,-0.144737267461644,
0.232799277269938));
#19102=CARTESIAN_POINT('Ctrl Pts',(-0.180808275411966,0.00865192846140473,
0.225039301360939));
#19103=CARTESIAN_POINT('Ctrl Pts',(-0.0942515706791253,0.154556313135293,
0.217279325451942));
#19104=CARTESIAN_POINT('Ctrl Pts',(0.0750450248431312,0.164716481511431,
0.209519349542944));
#19105=CARTESIAN_POINT('Ctrl Pts',(0.178461260043253,0.0303012077178856,
0.201759373633945));
#19106=CARTESIAN_POINT('Ctrl Pts',(0.125203781387627,-0.130731709675357,
0.193999397724948));
#19107=CARTESIAN_POINT('Ctrl Pts',(-0.0379704533096903,-0.17698585337688,
0.18623942181595));
#19108=CARTESIAN_POINT('Ctrl Pts',(-0.167810456277154,-0.0678671379413016,
0.178479445906952));
#19109=CARTESIAN_POINT('Ctrl Pts',(-0.150328180300649,0.100834978066992,
0.170719469997954));
#19110=CARTESIAN_POINT('Ctrl Pts',(-0.000871711368246156,0.181012066871201,
0.162959494088956));
#19111=CARTESIAN_POINT('Ctrl Pts',(0.149350085565286,0.102277888352765,
0.155199518179958));
#19112=CARTESIAN_POINT('Ctrl Pts',(0.168456255263351,-0.0662471829332422,
0.14743954227096));
#19113=CARTESIAN_POINT('Ctrl Pts',(0.0396733728729688,-0.17661315503135,
0.139679566361963));
#19114=CARTESIAN_POINT('Ctrl Pts',(-0.123939070884463,-0.131929162812062,
0.131919590452964));
#19115=CARTESIAN_POINT('Ctrl Pts',(-0.178744451066417,0.0285765376657333,
0.124159614543967));
#19116=CARTESIAN_POINT('Ctrl Pts',(-0.0766286530280003,0.163994611436961,
0.116399638634969));
#19117=CARTESIAN_POINT('Ctrl Pts',(0.0927599764682439,0.155440618724813,
0.108639662725971));
#19118=CARTESIAN_POINT('Ctrl Pts',(0.180714016146597,0.0104239566588842,
0.100879686816973));
#19119=CARTESIAN_POINT('Ctrl Pts',(0.11001758793024,-0.143743725357685,
0.093119710907975));
#19120=CARTESIAN_POINT('Ctrl Pts',(-0.0572637123892103,-0.171718146500831,
0.0853597349989769));
#19121=CARTESIAN_POINT('Ctrl Pts',(-0.174273565575645,-0.048938961879483,
0.0775997590899791));
#19122=CARTESIAN_POINT('Ctrl Pts',(-0.138285748054726,0.11680239511684,
0.0698397831809812));
#19123=CARTESIAN_POINT('Ctrl Pts',(0.0191012565771036,0.180005302104073,
0.0620798072719832));
#19124=CARTESIAN_POINT('Ctrl Pts',(0.159724738700703,0.0851738948996701,
0.0543198313629854));
#19125=CARTESIAN_POINT('Ctrl Pts',(0.160113920417758,-0.0844204212478698,
0.0465598554539874));
#19126=CARTESIAN_POINT('Ctrl Pts',(0.0199582426985643,-0.179924098035372,
0.0387998795449896));
#19127=CARTESIAN_POINT('Ctrl Pts',(-0.137757819841364,-0.117427728395404,
0.0310399036359917));
#19128=CARTESIAN_POINT('Ctrl Pts',(-0.174460933778308,0.0480767578110765,
0.0232799277269937));
#19129=CARTESIAN_POINT('Ctrl Pts',(-0.0581466660421577,0.171532975008042,
0.0155199518179959));
#19130=CARTESIAN_POINT('Ctrl Pts',(0.109502662757235,0.144085240745689,
0.00775997590899784));
#19131=CARTESIAN_POINT('Ctrl Pts',(0.156737212705124,0.0419221657566679,
0.00258665863633264));
#19132=CARTESIAN_POINT('Ctrl Pts',(0.15408394018464,-0.00816268198427004,
0.));
#19133=CARTESIAN_POINT('Ctrl Pts',(0.15408394018464,-0.00816268198427004,
0.));
#19134=CARTESIAN_POINT('Ctrl Pts',(0.153697863146473,0.00250812953454787,
1.45220469349306E-17));
#19135=CARTESIAN_POINT('Ctrl Pts',(0.152123106309386,0.0130673133993916,
-2.32988231788825E-17));
#19136=CARTESIAN_POINT('Ctrl Pts',(0.149466152202855,0.0233620190894148,
-6.07153216591882E-17));
#19137=CARTESIAN_POINT('Ctrl Pts',(0.14793019248835,0.0293132898222067,
-8.23454409684948E-17));
#19138=CARTESIAN_POINT('Ctrl Pts',(0.146031563681721,0.0351760135160456,
3.17823908273165E-17));
#19139=CARTESIAN_POINT('Ctrl Pts',(0.143784059453749,0.0409171473780902,
6.24500451351651E-17));
#19140=CARTESIAN_POINT('Ctrl Pts',(0.142595904075608,0.0439522291322952,
7.86626679846993E-17));
#19141=CARTESIAN_POINT('Ctrl Pts',(0.141309213132582,0.0469553015723855,
1.03399090950918E-16));
#19142=CARTESIAN_POINT('Ctrl Pts',(0.13992871365498,0.0499144025840292,
1.00613961606655E-16));
#19143=CARTESIAN_POINT('Ctrl Pts',(0.135493978469587,0.0594202586791481,
9.16669744478229E-17));
#19144=CARTESIAN_POINT('Ctrl Pts',(0.130119641392827,0.0684241765595774,
5.76730757846686E-17));
#19145=CARTESIAN_POINT('Ctrl Pts',(0.123887660540245,0.0767683201192124,
1.38777878078145E-16));
#19146=CARTESIAN_POINT('Ctrl Pts',(0.120656388342022,0.0810947453345699,
1.808305895663E-16));
#19147=CARTESIAN_POINT('Ctrl Pts',(0.117193874983239,0.0852432898306738,
1.062697842984E-16));
#19148=CARTESIAN_POINT('Ctrl Pts',(0.11350808038867,0.0891875047540603,
1.14491749414469E-16));
#19149=CARTESIAN_POINT('Ctrl Pts',(0.110158526423333,0.0927719043720516,
1.21963656801269E-16));
#19150=CARTESIAN_POINT('Ctrl Pts',(0.106618991420749,0.0961915975683434,
1.17223950247179E-16));
#19151=CARTESIAN_POINT('Ctrl Pts',(0.102922970874274,0.0994011657423757,
1.02348685082632E-16));
#19152=CARTESIAN_POINT('Ctrl Pts',(0.0973787571548163,0.104215676830788,
8.00350512245867E-17));
#19153=CARTESIAN_POINT('Ctrl Pts',(0.0914754811895955,0.108568278221023,
6.56075743842472E-17));
#19154=CARTESIAN_POINT('Ctrl Pts',(0.0852365492443714,0.11239450959967,
3.29597460435593E-17));
#19155=CARTESIAN_POINT('Ctrl Pts',(0.0787787796913796,0.116354950379705,
-7.26807264206779E-19));
#19156=CARTESIAN_POINT('Ctrl Pts',(0.0719608771003193,0.11975150351845,
7.81983513604452E-17));
#19157=CARTESIAN_POINT('Ctrl Pts',(0.0648645680501024,0.122569786811788,
1.05818132034585E-16));
#19158=CARTESIAN_POINT('Ctrl Pts',(0.0619760396963809,0.123716959397427,
1.17060669392563E-16));
#19159=CARTESIAN_POINT('Ctrl Pts',(0.0590419697559043,0.124767587801255,
-1.70921410850511E-17));
#19160=CARTESIAN_POINT('Ctrl Pts',(0.0560804949635964,0.12571697313192,
-8.67361737988404E-19));
#19161=CARTESIAN_POINT('Ctrl Pts',(0.0481895916857994,0.128246627558523,
4.23638569993146E-17));
#19162=CARTESIAN_POINT('Ctrl Pts',(0.040081547172159,0.13006877931966,2.48189907303608E-17));
#19163=CARTESIAN_POINT('Ctrl Pts',(0.0318655688619291,0.131172622122806,
0.));
#19164=CARTESIAN_POINT('Ctrl Pts',(0.0267717292715239,0.131856995664207,
-1.5387571972871E-17));
#19165=CARTESIAN_POINT('Ctrl Pts',(0.0216363184326117,0.132264755542675,
5.61228976213782E-17));
#19166=CARTESIAN_POINT('Ctrl Pts',(0.0164863123329273,0.132388468809724,
3.03576608295941E-17));
#19167=CARTESIAN_POINT('Ctrl Pts',(0.0120733572364389,0.13249447666326,
8.27985532573229E-18));
#19168=CARTESIAN_POINT('Ctrl Pts',(0.00764667637530932,0.132391154756805,
7.9933444120104E-17));
#19169=CARTESIAN_POINT('Ctrl Pts',(0.00324855819595315,0.132074892239241,
9.62771529167128E-17));
#19170=CARTESIAN_POINT('Ctrl Pts',(-0.00215998367955725,0.131685971569047,
1.16375665467493E-16));
#19171=CARTESIAN_POINT('Ctrl Pts',(-0.00753310453775717,0.130975837616781,
1.12286849362194E-16));
#19172=CARTESIAN_POINT('Ctrl Pts',(-0.0128378223015392,0.129936202211006,
1.27068494615301E-16));
#19173=CARTESIAN_POINT('Ctrl Pts',(-0.0180922709275414,0.128906418710228,
1.41710064449709E-16));
#19174=CARTESIAN_POINT('Ctrl Pts',(-0.023283936630727,0.12755123862641,
1.19281234835921E-16));
#19175=CARTESIAN_POINT('Ctrl Pts',(-0.028350637156304,0.125868914531291,
9.19403442267708E-17));
#19176=CARTESIAN_POINT('Ctrl Pts',(-0.0326437071621008,0.124443463179602,
6.87741127091605E-17));
#19177=CARTESIAN_POINT('Ctrl Pts',(-0.0368509055758185,0.122782751372096,
3.08039683582783E-17));
#19178=CARTESIAN_POINT('Ctrl Pts',(-0.0409513668396969,0.120880349084932,
-1.95156391047391E-18));
#19179=CARTESIAN_POINT('Ctrl Pts',(-0.0436523616789034,0.119627226953286,
-2.45035827619675E-17));
#19180=CARTESIAN_POINT('Ctrl Pts',(-0.0463070048384274,0.118269169850402,
-4.56986185075063E-18));
#19181=CARTESIAN_POINT('Ctrl Pts',(-0.0489111879062984,0.116810626195002,
-1.73472347597681E-18));
#19182=CARTESIAN_POINT('Ctrl Pts',(0.0958116152722397,0.0825211298936481,
0.24));
#19183=CARTESIAN_POINT('Ctrl Pts',(0.102494250906434,0.0762804363331629,
0.24));
#19184=CARTESIAN_POINT('Ctrl Pts',(0.108399952301676,0.0693089192431419,
0.24));
#19185=CARTESIAN_POINT('Ctrl Pts',(0.113520383394708,0.0617855200816623,
0.24));
#19186=CARTESIAN_POINT('Ctrl Pts',(0.11760088593285,0.0557900777417299,
0.24));
#19187=CARTESIAN_POINT('Ctrl Pts',(0.1211824537664,0.0494427873910869,0.24));
#19188=CARTESIAN_POINT('Ctrl Pts',(0.124247292533427,0.0428169095598754,
0.24));
#19189=CARTESIAN_POINT('Ctrl Pts',(0.125635784531567,0.0398151273949318,
0.24));
#19190=CARTESIAN_POINT('Ctrl Pts',(0.126914357096627,0.0367636074968772,
0.24));
#19191=CARTESIAN_POINT('Ctrl Pts',(0.128080244072735,0.0336751552254939,
0.24));
#19192=CARTESIAN_POINT('Ctrl Pts',(0.13155694143068,0.024465331227027,0.24));
#19193=CARTESIAN_POINT('Ctrl Pts',(0.134041462136676,0.0149150332268467,
0.24));
#19194=CARTESIAN_POINT('Ctrl Pts',(0.135496608205084,0.00520422800883078,
0.24));
#19195=CARTESIAN_POINT('Ctrl Pts',(0.136052940597398,0.00149158663520877,
0.24));
#19196=CARTESIAN_POINT('Ctrl Pts',(0.136458356591543,-0.00224482315054724,
0.24));
#19197=CARTESIAN_POINT('Ctrl Pts',(0.136708928272429,-0.00599574054845843,
0.24));
#19198=CARTESIAN_POINT('Ctrl Pts',(0.136894600108428,-0.00877514370161729,
0.24));
#19199=CARTESIAN_POINT('Ctrl Pts',(0.136994942037659,-0.0115613689854128,
0.24));
#19200=CARTESIAN_POINT('Ctrl Pts',(0.137008733057845,-0.0143405417274864,
0.24));
#19201=CARTESIAN_POINT('Ctrl Pts',(0.137045731231951,-0.0217964308202384,
0.24));
#19202=CARTESIAN_POINT('Ctrl Pts',(0.136462408227525,-0.0292204075226799,
0.24));
#19203=CARTESIAN_POINT('Ctrl Pts',(0.135240454646173,-0.0365388974416549,
0.24));
#19204=CARTESIAN_POINT('Ctrl Pts',(0.134058793448489,-0.0436160693529878,
0.24));
#19205=CARTESIAN_POINT('Ctrl Pts',(0.132280018312676,-0.050595007513092,
0.24));
#19206=CARTESIAN_POINT('Ctrl Pts',(0.129952822193542,-0.0574290655609092,
0.24));
#19207=CARTESIAN_POINT('Ctrl Pts',(0.128850070284018,-0.0606674134165377,
0.24));
#19208=CARTESIAN_POINT('Ctrl Pts',(0.127623182384127,-0.0638741644409745,
0.24));
#19209=CARTESIAN_POINT('Ctrl Pts',(0.126284110088584,-0.067028198101918,
0.24));
#19210=CARTESIAN_POINT('Ctrl Pts',(0.122654675969015,-0.0755769205431157,
0.24));
#19211=CARTESIAN_POINT('Ctrl Pts',(0.118195290975453,-0.0837663478860722,
0.24));
#19212=CARTESIAN_POINT('Ctrl Pts',(0.113014989178579,-0.0915013065162071,
0.24));
#19213=CARTESIAN_POINT('Ctrl Pts',(0.108985931714537,-0.0975172866704144,
0.24));
#19214=CARTESIAN_POINT('Ctrl Pts',(0.104519884911976,-0.103258562704539,
0.24));
#19215=CARTESIAN_POINT('Ctrl Pts',(0.0996546828651377,-0.108675969178894,
0.24));
#19216=CARTESIAN_POINT('Ctrl Pts',(0.0972822643803542,-0.11131765910988,
0.24));
#19217=CARTESIAN_POINT('Ctrl Pts',(0.09482095240722,-0.113875293456495,
0.24));
#19218=CARTESIAN_POINT('Ctrl Pts',(0.0922773332174137,-0.116342466058553,
0.24));
#19219=CARTESIAN_POINT('Ctrl Pts',(0.0868426048671788,-0.121613857680014,
0.24));
#19220=CARTESIAN_POINT('Ctrl Pts',(0.0810310485854155,-0.126474759557936,
0.24));
#19221=CARTESIAN_POINT('Ctrl Pts',(0.0748870600798396,-0.130870957562724,
0.24));
#19222=CARTESIAN_POINT('Ctrl Pts',(0.0715378781224404,-0.133267392228159,
0.24));
#19223=CARTESIAN_POINT('Ctrl Pts',(0.0680912231566627,-0.135524142754832,
0.24));
#19224=CARTESIAN_POINT('Ctrl Pts',(0.0645638484115253,-0.13762659390894,
0.24));
#19225=CARTESIAN_POINT('Ctrl Pts',(0.0598451535113139,-0.140439117742,0.24));
#19226=CARTESIAN_POINT('Ctrl Pts',(0.0549775790306604,-0.142978967531553,
0.24));
#19227=CARTESIAN_POINT('Ctrl Pts',(0.0499773507040556,-0.145225083935062,
0.24));
#19228=CARTESIAN_POINT('Ctrl Pts',(0.0466920976074369,-0.146700828718701,
0.24));
#19229=CARTESIAN_POINT('Ctrl Pts',(0.0433495270099635,-0.148049731670784,
0.24));
#19230=CARTESIAN_POINT('Ctrl Pts',(0.039956549802796,-0.149273502906639,
0.24));
#19231=CARTESIAN_POINT('Ctrl Pts',(-0.126296536029262,-6.10717992316628E-5,
0.159341967361942));
#19232=CARTESIAN_POINT('Ctrl Pts',(-0.12637083907321,-0.0163056929409037,
0.160361391877968));
#19233=CARTESIAN_POINT('Ctrl Pts',(-0.12344809088261,-0.0325245895549842,
0.161380816393994));
#19234=CARTESIAN_POINT('Ctrl Pts',(-0.117399968681154,-0.0474794518833934,
0.162400240910021));
#19235=CARTESIAN_POINT('Ctrl Pts',(-0.102053636235694,-0.0854254922118417,
0.164986899546353));
#19236=CARTESIAN_POINT('Ctrl Pts',(-0.0665853528586453,-0.115233359066084,
0.167573558182686));
#19237=CARTESIAN_POINT('Ctrl Pts',(-0.0265641275910804,-0.123819689910512,
0.170160216819019));
#19238=CARTESIAN_POINT('Ctrl Pts',(0.0134570976764845,-0.13240602075494,
0.172746875455351));
#19239=CARTESIAN_POINT('Ctrl Pts',(0.058031264834566,-0.119770815589554,
0.175333534091684));
#19240=CARTESIAN_POINT('Ctrl Pts',(0.0875924985281064,-0.0914586003428122,
0.177920192728017));
#19241=CARTESIAN_POINT('Ctrl Pts',(0.117153732221647,-0.0631463850960709,
0.180506851364349));
#19242=CARTESIAN_POINT('Ctrl Pts',(0.131702032450646,-0.0191571597679751,
0.183093510000682));
#19243=CARTESIAN_POINT('Ctrl Pts',(0.124851119980295,0.0211965060081854,
0.185680168637015));
#19244=CARTESIAN_POINT('Ctrl Pts',(0.118000207509943,0.0615501717843459,
0.188266827273347));
#19245=CARTESIAN_POINT('Ctrl Pts',(0.0897500823402403,0.0982682780085711,
0.19085348590968));
#19246=CARTESIAN_POINT('Ctrl Pts',(0.0525017161220023,0.115239608835997,
0.193440144546013));
#19247=CARTESIAN_POINT('Ctrl Pts',(0.0152533499037644,0.132210939663423,
0.196026803182345));
#19248=CARTESIAN_POINT('Ctrl Pts',(-0.030993257363009,0.129435495094051,
0.198613461818678));
#19249=CARTESIAN_POINT('Ctrl Pts',(-0.0659388717692058,0.108119484364762,
0.20120012045501));
#19250=CARTESIAN_POINT('Ctrl Pts',(-0.100884486175403,0.0868034736354726,
0.203786779091343));
#19251=CARTESIAN_POINT('Ctrl Pts',(-0.124529107721023,0.0469468967462671,
0.206373437727676));
#19252=CARTESIAN_POINT('Ctrl Pts',(-0.126492123469331,0.00606801008988057,
0.208960096364008));
#19253=CARTESIAN_POINT('Ctrl Pts',(-0.126588724127832,0.00405634646811867,
0.209087386696653));
#19254=CARTESIAN_POINT('Ctrl Pts',(-0.126632819376787,0.00204220716288977,
0.209214677029297));
#19255=CARTESIAN_POINT('Ctrl Pts',(-0.126625441102054,2.7778768752873E-5,
0.209341967361942));
#19256=CARTESIAN_POINT('Ctrl Pts',(-0.0398513841857245,-0.149064942821851,
0.24));
#19257=CARTESIAN_POINT('Ctrl Pts',(-0.0883048112969314,-0.136111285829332,
0.237413341363667));
#19258=CARTESIAN_POINT('Ctrl Pts',(-0.170871437255804,-0.0596187094618861,
0.232240024091002));
#19259=CARTESIAN_POINT('Ctrl Pts',(-0.145169204726118,0.108307533342445,
0.224480048182004));
#19260=CARTESIAN_POINT('Ctrl Pts',(0.00818767200092134,0.180778621679153,
0.216720072273006));
#19261=CARTESIAN_POINT('Ctrl Pts',(0.154249898498561,0.0947283641859207,
0.208960096364008));
#19262=CARTESIAN_POINT('Ctrl Pts',(0.164950538597243,-0.0745810526211722,
0.201200120455011));
#19263=CARTESIAN_POINT('Ctrl Pts',(0.0308106631569891,-0.178364693496558,
0.193440144546012));
#19264=CARTESIAN_POINT('Ctrl Pts',(-0.13036283225522,-0.125587074703769,
0.185680168637015));
#19265=CARTESIAN_POINT('Ctrl Pts',(-0.17709781441264,0.03745832727601,0.177920192728017));
#19266=CARTESIAN_POINT('Ctrl Pts',(-0.0683530255288039,0.167611467503216,
0.170160216819019));
#19267=CARTESIAN_POINT('Ctrl Pts',(0.100397202365132,0.150621028353064,
0.162400240910021));
#19268=CARTESIAN_POINT('Ctrl Pts',(0.18100910679194,0.00139719974911195,
0.154640265001023));
#19269=CARTESIAN_POINT('Ctrl Pts',(0.102711092909207,-0.149052183789333,
0.146880289092025));
#19270=CARTESIAN_POINT('Ctrl Pts',(-0.0657574679958034,-0.168648048308422,
0.139120313183027));
#19271=CARTESIAN_POINT('Ctrl Pts',(-0.176497206835689,-0.0401861834345609,
0.131360337274029));
#19272=CARTESIAN_POINT('Ctrl Pts',(-0.132288575936487,0.123555290563421,
0.123600361365031));
#19273=CARTESIAN_POINT('Ctrl Pts',(0.0280571680938306,0.178826694862324,
0.115840385456033));
#19274=CARTESIAN_POINT('Ctrl Pts',(0.163771354656592,0.0771047007047774,
0.108080409547035));
#19275=CARTESIAN_POINT('Ctrl Pts',(0.155709331479018,-0.0923080778690166,
0.100320433638038));
#19276=CARTESIAN_POINT('Ctrl Pts',(0.0109489686262093,-0.180682908560435,
0.0925604577290397));
#19277=CARTESIAN_POINT('Ctrl Pts',(-0.143423754439364,-0.110434756566834,
0.0848004818200417));
#19278=CARTESIAN_POINT('Ctrl Pts',(-0.17188331593326,0.0567648465404429,
0.0770405059110439));
#19279=CARTESIAN_POINT('Ctrl Pts',(-0.0494457976037486,0.174130301808973,
0.0692805300020459));
#19280=CARTESIAN_POINT('Ctrl Pts',(0.11640175885633,0.13862511662766,0.061520554093048));
#19281=CARTESIAN_POINT('Ctrl Pts',(0.18005704388064,-0.0185795878987759,
0.0537605781840501));
#19282=CARTESIAN_POINT('Ctrl Pts',(0.0856431484406112,-0.159474177462153,
0.0460006022750521));
#19283=CARTESIAN_POINT('Ctrl Pts',(-0.0839657292871194,-0.160363143120653,
0.0382406263660544));
#19284=CARTESIAN_POINT('Ctrl Pts',(-0.179844832231877,-0.0204718628801216,
0.0304806504570563));
#19285=CARTESIAN_POINT('Ctrl Pts',(-0.117866479118068,0.137399078213474,
0.0227206745480585));
#19286=CARTESIAN_POINT('Ctrl Pts',(0.0476444145610997,0.174632482457551,
0.0149606986390605));
#19287=CARTESIAN_POINT('Ctrl Pts',(0.171219786572432,0.0585809927800803,
0.00720072273006264));
#19288=CARTESIAN_POINT('Ctrl Pts',(0.144688050375066,-0.108949473877577,
-0.000559253178935319));
#19289=CARTESIAN_POINT('Ctrl Pts',(-0.0092814439579932,-0.180735423716049,
-0.00831922908793317));
#19290=CARTESIAN_POINT('Ctrl Pts',(-0.105867686800049,-0.122947365648507,
-0.0134925463605985));
#19291=CARTESIAN_POINT('Ctrl Pts',(-0.131895903200816,-0.0800747195988904,
-0.0160792049969312));
#19292=CARTESIAN_POINT('Ctrl Pts',(-0.0374537582415196,-0.140096572423086,
0.245359734998977));
#19293=CARTESIAN_POINT('Ctrl Pts',(-0.0829920245295529,-0.127922261611689,
0.242773076362644));
#19294=CARTESIAN_POINT('Ctrl Pts',(-0.160591096949962,-0.0560317985556137,
0.237599759089979));
#19295=CARTESIAN_POINT('Ctrl Pts',(-0.13643521822445,0.101791299158848,
0.229839783180981));
#19296=CARTESIAN_POINT('Ctrl Pts',(0.00769506740980954,0.1699022237233,
0.222079807271983));
#19297=CARTESIAN_POINT('Ctrl Pts',(0.144969579481095,0.0890291096113304,
0.214319831362985));
#19298=CARTESIAN_POINT('Ctrl Pts',(0.155026424317845,-0.0700939445729984,
0.206559855453987));
#19299=CARTESIAN_POINT('Ctrl Pts',(0.0289569648011409,-0.167633527556011,
0.19879987954499));
#19300=CARTESIAN_POINT('Ctrl Pts',(-0.122519659046519,-0.118031231043151,
0.191039903635991));
#19301=CARTESIAN_POINT('Ctrl Pts',(-0.166442869216287,0.0352046776440443,
0.183279927726994));
#19302=CARTESIAN_POINT('Ctrl Pts',(-0.064240621638164,0.157527260611955,
0.175519951817996));
#19303=CARTESIAN_POINT('Ctrl Pts',(0.0943568867767351,0.141559037340679,
0.167759975908998));
#19304=CARTESIAN_POINT('Ctrl Pts',(0.170118841887737,0.00131313836865665,
0.16));
#19305=CARTESIAN_POINT('Ctrl Pts',(0.0965315639882279,-0.140084581027326,
0.152240024091002));
#19306=CARTESIAN_POINT('Ctrl Pts',(-0.0618012237018238,-0.158501476380598,
0.144480048182004));
#19307=CARTESIAN_POINT('Ctrl Pts',(-0.165878396703103,-0.0377684145673052,
0.136720072273006));
#19308=CARTESIAN_POINT('Ctrl Pts',(-0.124329541933827,0.116121687534276,
0.128960096364008));
#19309=CARTESIAN_POINT('Ctrl Pts',(0.0263691315170036,0.168067732987372,
0.12120012045501));
#19310=CARTESIAN_POINT('Ctrl Pts',(0.153918185014798,0.0724657594331675,
0.113440144546012));
#19311=CARTESIAN_POINT('Ctrl Pts',(0.146341206869619,-0.0867544378416841,
0.105680168637015));
#19312=CARTESIAN_POINT('Ctrl Pts',(0.0102902328814698,-0.169812269106107,
0.0979201927280167));
#19313=CARTESIAN_POINT('Ctrl Pts',(-0.134794781526993,-0.103790539737311,
0.0901602168190187));
#19314=CARTESIAN_POINT('Ctrl Pts',(-0.161542096774173,0.0533496359633175,
0.0824002409100209));
#19315=CARTESIAN_POINT('Ctrl Pts',(-0.0464709316213242,0.163653894581969,
0.074640265001023));
#19316=CARTESIAN_POINT('Ctrl Pts',(0.109398542213106,0.130284849835523,
0.066880289092025));
#19317=CARTESIAN_POINT('Ctrl Pts',(0.16922405906302,-0.0174617621848401,
0.0591203131830272));
#19318=CARTESIAN_POINT('Ctrl Pts',(0.0804904984426183,-0.149879543972585,
0.0513603372740291));
#19319=CARTESIAN_POINT('Ctrl Pts',(-0.0789139998409189,-0.150715025739123,
0.0436003613650314));
#19320=CARTESIAN_POINT('Ctrl Pts',(-0.169024614954586,-0.0192401899891918,
0.0358403854560333));
#19321=CARTESIAN_POINT('Ctrl Pts',(-0.110775138777956,0.12913257502003,
0.0280804095470356));
#19322=CARTESIAN_POINT('Ctrl Pts',(0.0447779273164969,0.164125861942445,
0.0203204336380375));
#19323=CARTESIAN_POINT('Ctrl Pts',(0.16091848811479,0.0550565152494576,
0.0125604577290397));
#19324=CARTESIAN_POINT('Ctrl Pts',(0.135983012131502,-0.10239461786658,
0.00480048182004171));
#19325=CARTESIAN_POINT('Ctrl Pts',(-0.00872303347143,-0.169861624730324,
-0.00295949408895612));
#19326=CARTESIAN_POINT('Ctrl Pts',(-0.0994982439886826,-0.115550337924785,
-0.00813281136162148));
#19327=CARTESIAN_POINT('Ctrl Pts',(-0.123960494032221,-0.0752570895690155,
-0.0107194699979541));
#19328=CARTESIAN_POINT('Ctrl Pts',(-0.0350561322973148,-0.13112820202432,
0.250719469997954));
#19329=CARTESIAN_POINT('Ctrl Pts',(-0.0776792377621743,-0.119733237394047,
0.248132811361621));
#19330=CARTESIAN_POINT('Ctrl Pts',(-0.150310756644121,-0.0524448876493412,
0.242959494088956));
#19331=CARTESIAN_POINT('Ctrl Pts',(-0.127701231722781,0.0952750649752511,
0.235199518179958));
#19332=CARTESIAN_POINT('Ctrl Pts',(0.00720246281869772,0.159025825767447,
0.22743954227096));
#19333=CARTESIAN_POINT('Ctrl Pts',(0.135689260463629,0.08332985503674,0.219679566361962));
#19334=CARTESIAN_POINT('Ctrl Pts',(0.145102310038447,-0.0656068365248246,
0.211919590452964));
#19335=CARTESIAN_POINT('Ctrl Pts',(0.0271032664452926,-0.156902361615465,
0.204159614543967));
#19336=CARTESIAN_POINT('Ctrl Pts',(-0.114676485837817,-0.110475387382534,
0.196399638634969));
#19337=CARTESIAN_POINT('Ctrl Pts',(-0.155787924019933,0.0329510280120788,
0.188639662725971));
#19338=CARTESIAN_POINT('Ctrl Pts',(-0.0601282177475243,0.147443053720694,
0.180879686816973));
#19339=CARTESIAN_POINT('Ctrl Pts',(0.0883165711883383,0.132497046328295,
0.173119710907975));
#19340=CARTESIAN_POINT('Ctrl Pts',(0.159228576983534,0.00122907698820117,
0.165359734998977));
#19341=CARTESIAN_POINT('Ctrl Pts',(0.0903520350672485,-0.131116978265319,
0.157599759089979));
#19342=CARTESIAN_POINT('Ctrl Pts',(-0.0578449794078444,-0.148354904452775,
0.149839783180981));
#19343=CARTESIAN_POINT('Ctrl Pts',(-0.155259586570517,-0.0353506457000499,
0.142079807271983));
#19344=CARTESIAN_POINT('Ctrl Pts',(-0.116370507931168,0.108688084505131,
0.134319831362985));
#19345=CARTESIAN_POINT('Ctrl Pts',(0.0246810949401768,0.157308771112418,
0.126559855453988));
#19346=CARTESIAN_POINT('Ctrl Pts',(0.144065015373005,0.0678268181615582,
0.118799879544989));
#19347=CARTESIAN_POINT('Ctrl Pts',(0.13697308226022,-0.0812007978143519,
0.111039903635992));
#19348=CARTESIAN_POINT('Ctrl Pts',(0.00963149713673027,-0.15894162965178,
0.103279927726994));
#19349=CARTESIAN_POINT('Ctrl Pts',(-0.126165808614623,-0.0971463229077874,
0.0955199518179957));
#19350=CARTESIAN_POINT('Ctrl Pts',(-0.151200877615086,0.0499344253861922,
0.087759975908998));
#19351=CARTESIAN_POINT('Ctrl Pts',(-0.0434960656388994,0.153177487354966,
0.08));
#19352=CARTESIAN_POINT('Ctrl Pts',(0.102395325569881,0.121944583043386,
0.072240024091002));
#19353=CARTESIAN_POINT('Ctrl Pts',(0.158391074245402,-0.0163439364709043,
0.0644800481820042));
#19354=CARTESIAN_POINT('Ctrl Pts',(0.0753378484446251,-0.140284910483017,
0.0567200722730062));
#19355=CARTESIAN_POINT('Ctrl Pts',(-0.0738622703947183,-0.141066908357593,
0.0489600963640083));
#19356=CARTESIAN_POINT('Ctrl Pts',(-0.158204397677296,-0.018008517098262,
0.0412001204550104));
#19357=CARTESIAN_POINT('Ctrl Pts',(-0.103683798437843,0.120866071826586,
0.0334401445460125));
#19358=CARTESIAN_POINT('Ctrl Pts',(0.0419114400718942,0.153619241427338,
0.0256801686370146));
#19359=CARTESIAN_POINT('Ctrl Pts',(0.150617189657149,0.051532037718835,
0.0179201927280167));
#19360=CARTESIAN_POINT('Ctrl Pts',(0.127277973887939,-0.0958397618555833,
0.0101602168190187));
#19361=CARTESIAN_POINT('Ctrl Pts',(-0.00816462298486686,-0.1589878257446,
0.00240024091002091));
#19362=CARTESIAN_POINT('Ctrl Pts',(-0.0931288011773165,-0.108153310201063,
-0.00277307636264444));
#19363=CARTESIAN_POINT('Ctrl Pts',(-0.116025084863626,-0.0704394595391406,
-0.00535973499897709));
#19364=CARTESIAN_POINT('Ctrl Pts',(-0.0326585063531099,-0.122159831625555,
0.256079204996931));
#19365=CARTESIAN_POINT('Ctrl Pts',(-0.0723664509947957,-0.111544213176404,
0.253492546360598));
#19366=CARTESIAN_POINT('Ctrl Pts',(-0.140030416338279,-0.0488579767430688,
0.248319229087933));
#19367=CARTESIAN_POINT('Ctrl Pts',(-0.118967245221113,0.0887588307916541,
0.240559253178936));
#19368=CARTESIAN_POINT('Ctrl Pts',(0.00670985822758596,0.148149427811594,
0.232799277269937));
#19369=CARTESIAN_POINT('Ctrl Pts',(0.126408941446163,0.0776306004621497,
0.225039301360939));
#19370=CARTESIAN_POINT('Ctrl Pts',(0.13517819575905,-0.0611197284766509,
0.217279325451942));
#19371=CARTESIAN_POINT('Ctrl Pts',(0.0252495680894444,-0.146171195674918,
0.209519349542944));
#19372=CARTESIAN_POINT('Ctrl Pts',(-0.106833312629116,-0.102919543721916,
0.201759373633946));
#19373=CARTESIAN_POINT('Ctrl Pts',(-0.14513297882358,0.0306973783801131,
0.193999397724948));
#19374=CARTESIAN_POINT('Ctrl Pts',(-0.0560158138568844,0.137358846829434,
0.18623942181595));
#19375=CARTESIAN_POINT('Ctrl Pts',(0.0822762555999414,0.12343505531591,
0.178479445906952));
#19376=CARTESIAN_POINT('Ctrl Pts',(0.148338312079331,0.00114501560774606,
0.170719469997954));
#19377=CARTESIAN_POINT('Ctrl Pts',(0.0841725061462688,-0.122149375503312,
0.162959494088956));
#19378=CARTESIAN_POINT('Ctrl Pts',(-0.0538887351138648,-0.138208332524951,
0.155199518179959));
#19379=CARTESIAN_POINT('Ctrl Pts',(-0.144640776437932,-0.0329328768327946,
0.14743954227096));
#19380=CARTESIAN_POINT('Ctrl Pts',(-0.108411473928508,0.101254481475986,
0.139679566361963));
#19381=CARTESIAN_POINT('Ctrl Pts',(0.0229930583633497,0.146549809237466,
0.131919590452964));
#19382=CARTESIAN_POINT('Ctrl Pts',(0.134211845731212,0.0631878768899486,
0.124159614543967));
#19383=CARTESIAN_POINT('Ctrl Pts',(0.127604957650822,-0.0756471577870196,
0.116399638634969));
#19384=CARTESIAN_POINT('Ctrl Pts',(0.00897276139199077,-0.148070990197453,
0.108639662725971));
#19385=CARTESIAN_POINT('Ctrl Pts',(-0.117536835702253,-0.0905021060782641,
0.100879686816973));
#19386=CARTESIAN_POINT('Ctrl Pts',(-0.140859658455999,0.0465192148090667,
0.0931197109079749));
#19387=CARTESIAN_POINT('Ctrl Pts',(-0.0405211996564747,0.142701080127962,
0.0853597349989771));
#19388=CARTESIAN_POINT('Ctrl Pts',(0.0953921089266558,0.113604316251249,
0.077599759089979));
#19389=CARTESIAN_POINT('Ctrl Pts',(0.147558089427783,-0.0152261107569683,
0.0698397831809813));
#19390=CARTESIAN_POINT('Ctrl Pts',(0.070185198446632,-0.130690276993449,
0.0620798072719832));
#19391=CARTESIAN_POINT('Ctrl Pts',(-0.0688105409485176,-0.131418790976063,
0.0543198313629854));
#19392=CARTESIAN_POINT('Ctrl Pts',(-0.147384180400005,-0.0167768442073323,
0.0465598554539874));
#19393=CARTESIAN_POINT('Ctrl Pts',(-0.0965924580977301,0.112599568633142,
0.0387998795449896));
#19394=CARTESIAN_POINT('Ctrl Pts',(0.0390449528272914,0.143112620912232,
0.0310399036359916));
#19395=CARTESIAN_POINT('Ctrl Pts',(0.140315891199508,0.0480075601882123,
0.0232799277269937));
#19396=CARTESIAN_POINT('Ctrl Pts',(0.118572935644375,-0.0892849058445864,
0.0155199518179958));
#19397=CARTESIAN_POINT('Ctrl Pts',(-0.00760621249830358,-0.148114026758875,
0.00775997590899793));
#19398=CARTESIAN_POINT('Ctrl Pts',(-0.0867593583659504,-0.100756282477341,
0.00258665863633259));
#19399=CARTESIAN_POINT('Ctrl Pts',(-0.108089675695031,-0.0656218295092657,
-5.55111512312578E-17));
#19400=CARTESIAN_POINT('Ctrl Pts',(-0.108089675695031,-0.0656218295092657,
-5.55111512312578E-17));
#19401=CARTESIAN_POINT('Ctrl Pts',(-0.104219465379748,-0.0739058869203245,
-4.02841154597017E-17));
#19402=CARTESIAN_POINT('Ctrl Pts',(-0.0994141168358061,-0.0816768736924768,
-5.16144647363644E-17));
#19403=CARTESIAN_POINT('Ctrl Pts',(-0.0938412360364922,-0.088871564406415,
-3.81639164714898E-17));
#19404=CARTESIAN_POINT('Ctrl Pts',(-0.0894001862863345,-0.094605040600905,
-2.74451237748006E-17));
#19405=CARTESIAN_POINT('Ctrl Pts',(-0.0844703330957707,-0.0999727304469881,
3.12377098840079E-17));
#19406=CARTESIAN_POINT('Ctrl Pts',(-0.0791158513129458,-0.104935071387697,
-1.21430643318376E-17));
#19407=CARTESIAN_POINT('Ctrl Pts',(-0.0766900604813501,-0.107183206995485,
-3.17962611543325E-17));
#19408=CARTESIAN_POINT('Ctrl Pts',(-0.0741829996358932,-0.109342173006691,
4.83248416902999E-17));
#19409=CARTESIAN_POINT('Ctrl Pts',(-0.0716059924168524,-0.111405381598006,
5.3776427755281E-17));
#19410=CARTESIAN_POINT('Ctrl Pts',(-0.0639212992135713,-0.117557915794061,
7.00331794132204E-17));
#19411=CARTESIAN_POINT('Ctrl Pts',(-0.0556061968393146,-0.12287204611112,
-5.69073736333764E-18));
#19412=CARTESIAN_POINT('Ctrl Pts',(-0.0468203466856493,-0.127256781127915,
5.55111512312578E-17));
#19413=CARTESIAN_POINT('Ctrl Pts',(-0.0434613267337519,-0.12893315986732,
7.89099528597243E-17));
#19414=CARTESIAN_POINT('Ctrl Pts',(-0.0400330653128497,-0.130473352587733,
3.97002991909352E-17));
#19415=CARTESIAN_POINT('Ctrl Pts',(-0.0365431560942257,-0.131870761756357,
6.59194920871187E-17));
#19416=CARTESIAN_POINT('Ctrl Pts',(-0.0339571636773035,-0.13290622981212,
8.5347686277821E-17));
#19417=CARTESIAN_POINT('Ctrl Pts',(-0.0313383144727484,-0.133862652235137,
-2.74403076010104E-17));
#19418=CARTESIAN_POINT('Ctrl Pts',(-0.0286994266230122,-0.134734580282325,
-2.42861286636753E-17));
#19419=CARTESIAN_POINT('Ctrl Pts',(-0.0216199050576346,-0.137073760181214,
-1.58242011095522E-17));
#19420=CARTESIAN_POINT('Ctrl Pts',(-0.0143790427459088,-0.138813119073991,
5.80198461902811E-17));
#19421=CARTESIAN_POINT('Ctrl Pts',(-0.0070411538297537,-0.139912507657099,
6.93889390390723E-17));
#19422=CARTESIAN_POINT('Ctrl Pts',(5.47883476400097E-5,-0.140975646920361,
8.02325614020808E-17));
#19423=CARTESIAN_POINT('Ctrl Pts',(0.00724182591717642,-0.141440539972256,
1.32011341321413E-16));
#19424=CARTESIAN_POINT('Ctrl Pts',(0.0144605478337719,-0.141339082434075,
1.61329283265843E-16));
#19425=CARTESIAN_POINT('Ctrl Pts',(0.0178811722145177,-0.141291006315792,
1.75221724083914E-16));
#19426=CARTESIAN_POINT('Ctrl Pts',(0.021310106848269,-0.141115105569205,
1.85534911235541E-16));
#19427=CARTESIAN_POINT('Ctrl Pts',(0.0247235715439624,-0.140816220288761,
1.71737624121704E-16));
#19428=CARTESIAN_POINT('Ctrl Pts',(0.0339754553361668,-0.140006119078294,
1.34341339582434E-16));
#19429=CARTESIAN_POINT('Ctrl Pts',(0.0431421008898472,-0.138295657968001,
8.04496487960062E-17));
#19430=CARTESIAN_POINT('Ctrl Pts',(0.0520992976556894,-0.135759125106636,
3.20923843055709E-17));
#19431=CARTESIAN_POINT('Ctrl Pts',(0.0590658916121619,-0.13378629867842,
-5.518202506064E-18));
#19432=CARTESIAN_POINT('Ctrl Pts',(0.0659062642374416,-0.131312982137409,
7.87850579480063E-17));
#19433=CARTESIAN_POINT('Ctrl Pts',(0.0725619642951071,-0.128359965266718,
7.63278329429795E-17));
#19434=CARTESIAN_POINT('Ctrl Pts',(0.0758074813473741,-0.126919986522721,
7.51296170399226E-17));
#19435=CARTESIAN_POINT('Ctrl Pts',(0.0790005264283722,-0.125369490597537,
8.38688896655138E-17));
#19436=CARTESIAN_POINT('Ctrl Pts',(0.0821329715644795,-0.123712761836801,
7.24247051220317E-17));
#19437=CARTESIAN_POINT('Ctrl Pts',(0.0888257654942848,-0.120172989003949,
4.79730178566093E-17));
#19438=CARTESIAN_POINT('Ctrl Pts',(0.0952446087626691,-0.116147988031934,
8.96774285244103E-17));
#19439=CARTESIAN_POINT('Ctrl Pts',(0.101324221742587,-0.111663228753314,
8.28330459778925E-17));
#19440=CARTESIAN_POINT('Ctrl Pts',(0.104638321741973,-0.109218510516871,
7.91020571356516E-17));
#19441=CARTESIAN_POINT('Ctrl Pts',(0.107849695272814,-0.106637925639498,
3.17151869302413E-17));
#19442=CARTESIAN_POINT('Ctrl Pts',(0.110939265073957,-0.10393289123317,
1.53956708492942E-17));
#19443=CARTESIAN_POINT('Ctrl Pts',(0.115072333360666,-0.100314234708527,
-6.43574216607592E-18));
#19444=CARTESIAN_POINT('Ctrl Pts',(0.118992075260627,-0.0964697210975667,
5.54296751400654E-17));
#19445=CARTESIAN_POINT('Ctrl Pts',(0.122673447199167,-0.0924082746861152,
3.52365706057789E-17));
#19446=CARTESIAN_POINT('Ctrl Pts',(0.125092164655522,-0.0897398425098966,
2.31620156359627E-17));
#19447=CARTESIAN_POINT('Ctrl Pts',(0.127407959881093,-0.0869777021544565,
-4.01489640485901E-17));
#19448=CARTESIAN_POINT('Ctrl Pts',(0.129620323775263,-0.0841289546921697,
-3.98986399474666E-17));
#19449=CARTESIAN_POINT('Ctrl Pts',(-0.126471935391749,0.000101176582396995,
0.195658032638058));
#19450=CARTESIAN_POINT('Ctrl Pts',(-0.126547267107008,0.00888033934128026,
0.195105154333688));
#19451=CARTESIAN_POINT('Ctrl Pts',(-0.125707148272093,0.0176451944231377,
0.194552276029318));
#19452=CARTESIAN_POINT('Ctrl Pts',(-0.12389684029672,0.0262048027713284,
0.193999397724948));
#19453=CARTESIAN_POINT('Ctrl Pts',(-0.115427257168015,0.0662512011965534,
0.191412739088615));
#19454=CARTESIAN_POINT('Ctrl Pts',(-0.0857215355124495,0.101805024012994,
0.188826080452282));
#19455=CARTESIAN_POINT('Ctrl Pts',(-0.0478199964418627,0.117261303502293,
0.18623942181595));
#19456=CARTESIAN_POINT('Ctrl Pts',(-0.0099184573712758,0.132717582991593,
0.183652763179617));
#19457=CARTESIAN_POINT('Ctrl Pts',(0.0361788991143328,0.128076319153751,
0.181066104543285));
#19458=CARTESIAN_POINT('Ctrl Pts',(0.070237920103702,0.105374013950137,
0.178479445906952));
#19459=CARTESIAN_POINT('Ctrl Pts',(0.104296941093071,0.0826717087465222,
0.175892787270619));
#19460=CARTESIAN_POINT('Ctrl Pts',(0.126317626586201,0.0419083621771342,
0.173306128634287));
#19461=CARTESIAN_POINT('Ctrl Pts',(0.126633668343922,0.000977623707263797,
0.170719469997954));
#19462=CARTESIAN_POINT('Ctrl Pts',(0.126949710101644,-0.0399531147626067,
0.168132811361621));
#19463=CARTESIAN_POINT('Ctrl Pts',(0.105561108123956,-0.08105124513296,
0.165546152725289));
#19464=CARTESIAN_POINT('Ctrl Pts',(0.0718566002584231,-0.104276803155076,
0.162959494088956));
#19465=CARTESIAN_POINT('Ctrl Pts',(0.0381520923928904,-0.127502361177192,
0.160372835452623));
#19466=CARTESIAN_POINT('Ctrl Pts',(-0.00786832136048696,-0.132855346851071,
0.157786176816291));
#19467=CARTESIAN_POINT('Ctrl Pts',(-0.0460038684578537,-0.117985930405985,
0.155199518179958));
#19468=CARTESIAN_POINT('Ctrl Pts',(-0.0841394155552204,-0.103116513960899,
0.152612859543626));
#19469=CARTESIAN_POINT('Ctrl Pts',(-0.114390095996576,-0.0680246953968468,
0.150026200907293));
#19470=CARTESIAN_POINT('Ctrl Pts',(-0.12347721913235,-0.0281142263966907,
0.14743954227096));
#19471=CARTESIAN_POINT('Ctrl Pts',(-0.125563410841138,-0.018951712774069,
0.14684570572666));
#19472=CARTESIAN_POINT('Ctrl Pts',(-0.126534167537385,-0.00953522996602069,
0.146251869182359));
#19473=CARTESIAN_POINT('Ctrl Pts',(-0.126453631260982,-0.000102348163238207,
0.145658032638058));
#19474=CARTESIAN_POINT('Ctrl Pts',(-0.0398513841857245,-0.149064942821851,
0.24));
#19475=CARTESIAN_POINT('Ctrl Pts',(-0.0498806325786677,-0.145400296738327,
0.24));
#19476=CARTESIAN_POINT('Ctrl Pts',(-0.0594363948008725,-0.140639648297949,
0.24));
#19477=CARTESIAN_POINT('Ctrl Pts',(-0.0684062055177017,-0.134931499399492,
0.24));
#19478=CARTESIAN_POINT('Ctrl Pts',(-0.0735915624001909,-0.131631676235849,
0.24));
#19479=CARTESIAN_POINT('Ctrl Pts',(-0.0785806353345173,-0.128014298080738,
0.24));
#19480=CARTESIAN_POINT('Ctrl Pts',(-0.0833462611484583,-0.124102693747304,
0.24));
#19481=CARTESIAN_POINT('Ctrl Pts',(-0.0858656342542594,-0.122034803580736,
0.24));
#19482=CARTESIAN_POINT('Ctrl Pts',(-0.0883241156266364,-0.11988309220465,
0.24));
#19483=CARTESIAN_POINT('Ctrl Pts',(-0.0907117892851122,-0.117655751751618,
0.24));
#19484=CARTESIAN_POINT('Ctrl Pts',(-0.0983819858496404,-0.110500611839494,
0.24));
#19485=CARTESIAN_POINT('Ctrl Pts',(-0.105284458416918,-0.102606966330569,
0.24));
#19486=CARTESIAN_POINT('Ctrl Pts',(-0.111294422020379,-0.0941015332659665,
0.24));
#19487=CARTESIAN_POINT('Ctrl Pts',(-0.114410577497229,-0.0896914812962706,
0.24));
#19488=CARTESIAN_POINT('Ctrl Pts',(-0.117286101138547,-0.0851164738413172,
0.24));
#19489=CARTESIAN_POINT('Ctrl Pts',(-0.119898298320422,-0.0803922539627851,
0.24));
#19490=CARTESIAN_POINT('Ctrl Pts',(-0.1222721977331,-0.0760990011896685,
0.24));
#19491=CARTESIAN_POINT('Ctrl Pts',(-0.124430744329062,-0.0716759619599862,
0.24));
#19492=CARTESIAN_POINT('Ctrl Pts',(-0.126341093034125,-0.0671690272221462,
0.24));
#19493=CARTESIAN_POINT('Ctrl Pts',(-0.129206708925078,-0.060408406100978,
0.24));
#19494=CARTESIAN_POINT('Ctrl Pts',(-0.131522065955468,-0.0534490321795157,
0.24));
#19495=CARTESIAN_POINT('Ctrl Pts',(-0.133233091500091,-0.0463330844490581,
0.24));
#19496=CARTESIAN_POINT('Ctrl Pts',(-0.135004134506116,-0.0389675313754268,
0.24));
#19497=CARTESIAN_POINT('Ctrl Pts',(-0.136127599829873,-0.0314337185245799,
0.24));
#19498=CARTESIAN_POINT('Ctrl Pts',(-0.136615064298196,-0.0238138180582873,
0.24));
#19499=CARTESIAN_POINT('Ctrl Pts',(-0.136813484749433,-0.0207121682209076,
0.24));
#19500=CARTESIAN_POINT('Ctrl Pts',(-0.136906013213758,-0.0175970392000076,
0.24));
#19501=CARTESIAN_POINT('Ctrl Pts',(-0.136893785357156,-0.0144871321155608,
0.24));
#19502=CARTESIAN_POINT('Ctrl Pts',(-0.136861203984761,-0.00620072149302863,
0.24));
#19503=CARTESIAN_POINT('Ctrl Pts',(-0.136088646936857,0.00207357465703332,
0.24));
#19504=CARTESIAN_POINT('Ctrl Pts',(-0.134599584032292,0.0102285531249486,
0.24));
#19505=CARTESIAN_POINT('Ctrl Pts',(-0.133676409755049,0.0152843948425598,
0.24));
#19506=CARTESIAN_POINT('Ctrl Pts',(-0.132477333465274,0.0202942984003417,
0.24));
#19507=CARTESIAN_POINT('Ctrl Pts',(-0.131003622030167,0.0252303138624672,
0.24));
#19508=CARTESIAN_POINT('Ctrl Pts',(-0.129740734874544,0.029460199292259,
0.24));
#19509=CARTESIAN_POINT('Ctrl Pts',(-0.128274507607502,0.0336384499732856,
0.24));
#19510=CARTESIAN_POINT('Ctrl Pts',(-0.126614574688298,0.0377237273426867,
0.24));
#19511=CARTESIAN_POINT('Ctrl Pts',(-0.124573382985647,0.042747324485064,
0.24));
#19512=CARTESIAN_POINT('Ctrl Pts',(-0.122237651925267,0.0476379767326878,
0.24));
#19513=CARTESIAN_POINT('Ctrl Pts',(-0.119609691052418,0.0523617558795304,
0.24));
#19514=CARTESIAN_POINT('Ctrl Pts',(-0.117006563775536,0.0570408964535612,
0.24));
#19515=CARTESIAN_POINT('Ctrl Pts',(-0.114113358229268,0.0615597689541448,
0.24));
#19516=CARTESIAN_POINT('Ctrl Pts',(-0.110947628485839,0.0658586917144141,
0.24));
#19517=CARTESIAN_POINT('Ctrl Pts',(-0.108265305855902,0.0695011687224882,
0.24));
#19518=CARTESIAN_POINT('Ctrl Pts',(-0.105385772272888,0.0729892759232728,
0.24));
#19519=CARTESIAN_POINT('Ctrl Pts',(-0.102309360287629,0.0763011815833395,
0.24));
#19520=CARTESIAN_POINT('Ctrl Pts',(-0.100282916666232,0.0784827457339379,
0.24));
#19521=CARTESIAN_POINT('Ctrl Pts',(-0.0981709975111385,0.0805877996091198,
0.24));
#19522=CARTESIAN_POINT('Ctrl Pts',(-0.0959791030802606,0.0826138105732947,
0.24));
#19523=CARTESIAN_POINT('Origin',(0.,0.,0.24));
#19524=CARTESIAN_POINT('',(0.158771324027147,-0.275,0.24));
#19525=CARTESIAN_POINT('',(0.317542648054294,0.,0.24));
#19526=CARTESIAN_POINT('',(0.158771324027147,-0.275,0.24));
#19527=CARTESIAN_POINT('',(0.158771324027147,0.275,0.24));
#19528=CARTESIAN_POINT('',(0.317542648054294,0.,0.24));
#19529=CARTESIAN_POINT('',(-0.158771324027147,0.275,0.24));
#19530=CARTESIAN_POINT('',(0.158771324027147,0.275,0.24));
#19531=CARTESIAN_POINT('',(-0.317542648054294,5.55111512312578E-17,0.24));
#19532=CARTESIAN_POINT('',(-0.158771324027147,0.275,0.24));
#19533=CARTESIAN_POINT('',(-0.158771324027147,-0.275,0.24));
#19534=CARTESIAN_POINT('',(-0.317542648054294,3.88877587532466E-17,0.24));
#19535=CARTESIAN_POINT('',(-0.158771324027147,-0.275,0.24));
#19536=CARTESIAN_POINT('Origin',(0.,0.,0.12));
#19537=CARTESIAN_POINT('Origin',(-0.158771324027147,-0.275,0.));
#19538=CARTESIAN_POINT('',(-0.158771324027147,-0.275,0.));
#19539=CARTESIAN_POINT('',(0.158771324027147,-0.275,0.));
#19540=CARTESIAN_POINT('',(-0.158771324027147,-0.275,0.));
#19541=CARTESIAN_POINT('',(0.158771324027147,-0.275,0.));
#19542=CARTESIAN_POINT('',(-0.158771324027147,-0.275,0.));
#19543=CARTESIAN_POINT('Origin',(-0.317542648054294,3.88877587532466E-17,
0.));
#19544=CARTESIAN_POINT('',(-0.317542648054294,3.88877587532466E-17,0.));
#19545=CARTESIAN_POINT('',(-0.317542648054294,3.88877587532466E-17,0.));
#19546=CARTESIAN_POINT('',(-0.317542648054294,3.88877587532466E-17,0.));
#19547=CARTESIAN_POINT('Origin',(-0.158771324027147,0.275,0.));
#19548=CARTESIAN_POINT('',(-0.158771324027147,0.275,0.));
#19549=CARTESIAN_POINT('',(-0.158771324027147,0.275,0.));
#19550=CARTESIAN_POINT('',(-0.158771324027147,0.275,0.));
#19551=CARTESIAN_POINT('Origin',(0.158771324027147,0.275,0.));
#19552=CARTESIAN_POINT('',(0.158771324027147,0.275,0.));
#19553=CARTESIAN_POINT('',(0.158771324027147,0.275,0.));
#19554=CARTESIAN_POINT('',(0.158771324027147,0.275,0.));
#19555=CARTESIAN_POINT('Origin',(0.317542648054294,0.,0.));
#19556=CARTESIAN_POINT('',(0.317542648054294,0.,0.));
#19557=CARTESIAN_POINT('',(0.317542648054294,0.,0.));
#19558=CARTESIAN_POINT('',(0.317542648054294,0.,0.));
#19559=CARTESIAN_POINT('Origin',(0.158771324027147,-0.275,0.));
#19560=CARTESIAN_POINT('',(0.158771324027147,-0.275,0.));
#19561=CARTESIAN_POINT('Origin',(0.,0.,0.));
#19603=UNCERTAINTY_MEASURE_WITH_UNIT(LENGTH_MEASURE(0.001),#19619,
'DISTANCE_ACCURACY_VALUE',
'Maximum model space distance between geometric entities at asserted c
onnectivities');
#19605=UNCERTAINTY_MEASURE_WITH_UNIT(LENGTH_MEASURE(0.001),#19619,
'DISTANCE_ACCURACY_VALUE',
'Maximum model space distance between geometric entities at asserted c
onnectivities');
#19616=(
GEOMETRIC_REPRESENTATION_CONTEXT(3)
GLOBAL_UNCERTAINTY_ASSIGNED_CONTEXT((#19603))
GLOBAL_UNIT_ASSIGNED_CONTEXT((#19619,#19621,#19622))
REPRESENTATION_CONTEXT('','3D')
);
#19618=(
GEOMETRIC_REPRESENTATION_CONTEXT(3)
GLOBAL_UNCERTAINTY_ASSIGNED_CONTEXT((#19605))
GLOBAL_UNIT_ASSIGNED_CONTEXT((#19619,#19621,#19622))
REPRESENTATION_CONTEXT('','3D')
);
#19619=(
LENGTH_UNIT()
NAMED_UNIT(*)
SI_UNIT(.CENTI.,.METRE.)
);
#19621=(
NAMED_UNIT(*)
PLANE_ANGLE_UNIT()
SI_UNIT($,.RADIAN.)
);
#19622=(
NAMED_UNIT(*)
SI_UNIT($,.STERADIAN.)
SOLID_ANGLE_UNIT()
);
#19633=SHAPE_DEFINITION_REPRESENTATION(#19645,#19673);
#19645=PRODUCT_DEFINITION_SHAPE('',$,#19686);
#19673=SHAPE_REPRESENTATION('',(#7718),#19616);
#19675=PRODUCT_DEFINITION_CONTEXT('part definition',#19713,'design');
#19686=PRODUCT_DEFINITION('2026-11-10-01-34-59-968','Hex nut M3',#19698,
#19675);
#19698=PRODUCT_DEFINITION_FORMATION('',$,#19725);
#19713=APPLICATION_CONTEXT(
'Core Data for Automotive Mechanical Design Process');
#19714=PRODUCT_CONTEXT('part definition',#19713,'mechanical');
#19725=PRODUCT('2026-11-10-01-34-59-968','Hex nut M3',$,(#19714));
#19733=PRESENTATION_STYLE_ASSIGNMENT((#19741));
#19741=SURFACE_STYLE_USAGE(.BOTH.,#19749);
#19749=SURFACE_SIDE_STYLE('',(#19757));
#19757=SURFACE_STYLE_FILL_AREA(#19765);
#19765=FILL_AREA_STYLE('Fastener gray',(#19773));
#19773=FILL_AREA_STYLE_COLOUR('Fastener gray',#19781);
#19781=COLOUR_RGB('Fastener gray',0.607843137254902,0.643137254901961,0.698039215686274);
ENDSEC;
END-ISO-10303-21;
